ISO-10303-21;
HEADER;
FILE_DESCRIPTION (('STEP AP214'),
    '1' );
FILE_NAME ('hex bolt gradeab_iso_ISO 4014 - M10 x 45 x 26-N.step',
    '2026-10-10T03:43:58',
    ( '' ),
    ( '' ),
    'SwSTEP 2.0',
    'SolidWorks 2026',
    '' );
FILE_SCHEMA (( 'AUTOMOTIVE_DESIGN' ));
ENDSEC;

DATA;
#102=ORIENTED_EDGE ( 'NONE', *, *, #65193, .F. ) ;
#109=CIRCLE ( 'NONE', #32707, 5.400000000000001243 ) ;
#143=CARTESIAN_POINT ( 'NONE',  ( 6.400000000000000355, -9.237604307034018802, 3.355146209984123968E-17 ) ) ;
#305=DIRECTION ( 'NONE',  ( 0.000000000000000000, 0.000000000000000000, 1.000000000000000000 ) ) ;
#315=DIRECTION ( 'NONE',  ( 0.000000000000000000, 0.000000000000000000, -1.000000000000000000 ) ) ;
#334=ORIENTED_EDGE ( 'NONE', *, *, #37544, .F. ) ;
#338=CARTESIAN_POINT ( 'NONE',  ( 0.000000000000000000, 6.123233995736767268E-16, -5.000000000000000888 ) ) ;
#339=CARTESIAN_POINT ( 'NONE',  ( 0.08285530294364991388, 1.570896314703519092, -8.000000000000000000 ) ) ;
#412=CARTESIAN_POINT ( 'NONE',  ( 6.800000000000000711, 0.000000000000000000, 0.000000000000000000 ) ) ;
#548=DIRECTION ( 'NONE',  ( 0.000000000000000000, -0.5000000000000013323, -0.8660254037844379305 ) ) ;
#610=CARTESIAN_POINT ( 'NONE',  ( 50.57199999999998852, 0.000000000000000000, 5.000000000000000888 ) ) ;
#622=VECTOR ( 'NONE', #43796, 1000.000000000000000 ) ;
#802=CARTESIAN_POINT ( 'NONE',  ( 6.800000000000000711, 0.000000000000000000, 0.000000000000000000 ) ) ;
#851=CARTESIAN_POINT ( 'NONE',  ( 0.000000000000000000, 0.000000000000000000, 0.000000000000000000 ) ) ;
#886=CARTESIAN_POINT ( 'NONE',  ( 0.06730325657375685333, -1.557442666578433776, -8.000000000000000000 ) ) ;
#946=CARTESIAN_POINT ( 'NONE',  ( 6.800000000000000711, 0.000000000000000000, 5.000000000000000888 ) ) ;
#1151=CARTESIAN_POINT ( 'NONE',  ( 0.000000000000000000, -6.928203230275503444, 4.000000000000010658 ) ) ;
#1219=CARTESIAN_POINT ( 'NONE',  ( 5.799999999999999822, 0.000000000000000000, 0.000000000000000000 ) ) ;
#1485=AXIS2_PLACEMENT_3D ( 'NONE', #851, #39193, #44812 ) ;
#1531=EDGE_LOOP ( 'NONE', ( #47811, #17635, #2209 ) ) ;
#1564=DIRECTION ( 'NONE',  ( 0.000000000000000000, 0.000000000000000000, 1.000000000000000000 ) ) ;
#1650=DIRECTION ( 'NONE',  ( 0.000000000000000000, 0.000000000000000000, -1.000000000000000000 ) ) ;
#1669=ORIENTED_EDGE ( 'NONE', *, *, #37017, .F. ) ;
#1702=ORIENTED_EDGE ( 'NONE', *, *, #53762, .T. ) ;
#1746=EDGE_LOOP ( 'NONE', ( #27404, #16430, #22724, #24439 ) ) ;
#1851=ORIENTED_EDGE ( 'NONE', *, *, #49528, .F. ) ;
#1869=EDGE_LOOP ( 'NONE', ( #22751, #69273, #8707 ) ) ;
#1890=CARTESIAN_POINT ( 'NONE',  ( 0.1306530452038070222, -5.952467836904146381, 5.690023276062398772 ) ) ;
#1967=ORIENTED_EDGE ( 'NONE', *, *, #20792, .F. ) ;
#2015=DIRECTION ( 'NONE',  ( -1.000000000000000000, -0.000000000000000000, -0.000000000000000000 ) ) ;
#2022=CARTESIAN_POINT ( 'NONE',  ( 0.7145311798163268557, -9.237604307034018802, 5.946466066724412554E-16 ) ) ;
#2068=ADVANCED_FACE ( 'NONE', ( #27572 ), #28452, .T. ) ;
#2156=PLANE ( 'NONE',  #68079 ) ;
#2209=ORIENTED_EDGE ( 'NONE', *, *, #12961, .T. ) ;
#2227=VERTEX_POINT ( 'NONE', #53524 ) ;
#2349=CIRCLE ( 'NONE', #4590, 8.000000000000000000 ) ;
#2709=ORIENTED_EDGE ( 'NONE', *, *, #35169, .F. ) ;
#2759=ORIENTED_EDGE ( 'NONE', *, *, #7249, .T. ) ;
#2848=ORIENTED_EDGE ( 'NONE', *, *, #52436, .F. ) ;
#2971=CARTESIAN_POINT ( 'NONE',  ( 5.799999999999999822, 8.000000000000000000, 0.000000000000000000 ) ) ;
#3001=LINE ( 'NONE', #61038, #52882 ) ;
#3023=DIRECTION ( 'NONE',  ( 0.000000000000000000, 0.000000000000000000, 1.000000000000000000 ) ) ;
#3037=ADVANCED_FACE ( 'NONE', ( #44100 ), #56068, .T. ) ;
#3056=CARTESIAN_POINT ( 'NONE',  ( 6.400000000000000355, 9.237604307034018802, 0.000000000000000000 ) ) ;
#3059=CARTESIAN_POINT ( 'NONE',  ( 0.1306530452038120182, -7.903938623646872941, -2.309976723937608334 ) ) ;
#3076=ORIENTED_EDGE ( 'NONE', *, *, #18911, .F. ) ;
#3368=CARTESIAN_POINT ( 'NONE',  ( -3.806566064960824935E-15, 7.321656987762869662, -3.318518101603011417 ) ) ;
#3484=EDGE_LOOP ( 'NONE', ( #44919, #29130, #61279, #39171, #29061, #39628 ) ) ;
#3709=DIRECTION ( 'NONE',  ( 1.000000000000000000, 0.000000000000000000, 0.000000000000000000 ) ) ;
#3777=CIRCLE ( 'NONE', #61078, 4.171999999999999709 ) ;
#3886=CARTESIAN_POINT ( 'NONE',  ( 0.000000000000000000, 0.000000000000000000, 0.000000000000000000 ) ) ;
#3902=SURFACE_SIDE_STYLE ('',( #14792 ) ) ;
#3908=ORIENTED_EDGE ( 'NONE', *, *, #60509, .T. ) ;
#3999=DIRECTION ( 'NONE',  ( -1.000000000000000000, -0.000000000000000000, -0.000000000000000000 ) ) ;
#4071=ADVANCED_FACE ( 'NONE', ( #20505 ), #5928, .T. ) ;
#4131=VECTOR ( 'NONE', #2015, 1000.000000000000000 ) ;
#4172=CARTESIAN_POINT ( 'NONE',  ( 5.799999999999999822, -6.928203230275509661, -3.999999999999998224 ) ) ;
#4181=DIRECTION ( 'NONE',  ( -1.000000000000000000, 0.000000000000000000, -0.000000000000000000 ) ) ;
#4224=CARTESIAN_POINT ( 'NONE',  ( 5.799999999999999822, 4.618802153517001408, -8.000000000000000000 ) ) ;
#4357=CARTESIAN_POINT ( 'NONE',  ( 0.7145311798163274108, 9.237604307034018802, -2.124379920709345337E-16 ) ) ;
#4454=CARTESIAN_POINT ( 'NONE',  ( 5.799999999999999822, 9.237604307034018802, 0.000000000000000000 ) ) ;
#4481=CARTESIAN_POINT ( 'NONE',  ( 0.1306530452038078272, 5.952467836904149934, -5.690023276062396107 ) ) ;
#4590=AXIS2_PLACEMENT_3D ( 'NONE', #44668, #50982, #20015 ) ;
#4709=CARTESIAN_POINT ( 'NONE',  ( 0.4973051450695264442, -3.866309095700703136, 8.000000000000000000 ) ) ;
#4827=CARTESIAN_POINT ( 'NONE',  ( 0.000000000000000000, 6.928203230275505220, -4.000000000000007994 ) ) ;
#4935=CARTESIAN_POINT ( 'NONE',  ( 0.01678220608715907600, 0.7854258608507247441, -8.000000000000001776 ) ) ;
#4983=VECTOR ( 'NONE', #548, 1000.000000000000000 ) ;
#5086=AXIS2_PLACEMENT_3D ( 'NONE', #62696, #14496, #46851 ) ;
#5223=DIRECTION ( 'NONE',  ( 1.000000000000000000, 0.000000000000000000, -0.000000000000000000 ) ) ;
#5293=CARTESIAN_POINT ( 'NONE',  ( 5.799999999999999822, -9.237604307034018802, 3.355146209984123968E-17 ) ) ;
#5574=DIRECTION ( 'NONE',  ( -1.000000000000000000, -0.000000000000000000, -0.000000000000000000 ) ) ;
#5616=CARTESIAN_POINT ( 'NONE',  ( 0.3194001229792609031, 3.115132258397515397, -7.999999999999996447 ) ) ;
#5799=EDGE_LOOP ( 'NONE', ( #66770, #47407, #20325 ) ) ;
#5884=CIRCLE ( 'NONE', #20449, 8.000000000000000000 ) ;
#5928=CONICAL_SURFACE ( 'NONE', #50897, 8.000000000000000000, 1.047197551196600296 ) ;
#5970=DIRECTION ( 'NONE',  ( -1.000000000000000000, -0.000000000000000000, -0.000000000000000000 ) ) ;
#6076=AXIS2_PLACEMENT_3D ( 'NONE', #412, #39114, #12366 ) ;
#6085=FACE_OUTER_BOUND ( 'NONE', #8427, .T. ) ;
#6178=DIRECTION ( 'NONE',  ( 0.000000000000000000, -0.4999999999999998890, 0.8660254037844387076 ) ) ;
#6451=CARTESIAN_POINT ( 'NONE',  ( 0.000000000000000000, 0.000000000000000000, 0.000000000000000000 ) ) ;
#6526=B_SPLINE_CURVE_WITH_KNOTS ( 'NONE', 3,
 ( #40331, #35059, #7981, #12923, #3059, #29432, #35760, #2022 ),
 .UNSPECIFIED., .F., .F.,
 ( 4, 2, 2, 4 ),
 ( 0.004673709593152156581, 0.005837709341827646004, 0.007001709090503134558, 0.009329708587854115137 ),
 .UNSPECIFIED. ) ;
#6590=DIRECTION ( 'NONE',  ( -0.000000000000000000, 1.000000000000000000, 1.877893248421448789E-16 ) ) ;
#6670=CARTESIAN_POINT ( 'NONE',  ( 5.799999999999999822, -9.237604307034018802, 0.000000000000000000 ) ) ;
#6735=CARTESIAN_POINT ( 'NONE',  ( 6.400000000000000355, 9.797174393178825657E-16, -8.000000000000000000 ) ) ;
#6777=VERTEX_POINT ( 'NONE', #37148 ) ;
#6854=CARTESIAN_POINT ( 'NONE',  ( 5.260074602449203133E-16, -0.7818963811860513147, -8.000000000000000000 ) ) ;
#6878=ORIENTED_EDGE ( 'NONE', *, *, #37544, .T. ) ;
#6893=CARTESIAN_POINT ( 'NONE',  ( 0.3167204509598363082, 5.377136764700156668, 6.686525924292793022 ) ) ;
#6934=EDGE_CURVE ( 'NONE', #15138, #69105, #23030, .T. ) ;
#6958=AXIS2_PLACEMENT_3D ( 'NONE', #48119, #36556, #41489 ) ;
#7249=EDGE_CURVE ( 'NONE', #9445, #46646, #28705, .T. ) ;
#7361=AXIS2_PLACEMENT_3D ( 'NONE', #30135, #58233, #63515 ) ;
#7491=ADVANCED_FACE ( 'NONE', ( #14425 ), #9146, .T. ) ;
#7725=ORIENTED_EDGE ( 'NONE', *, *, #8877, .T. ) ;
#7818=ADVANCED_FACE ( 'NONE', ( #45477 ), #22635, .T. ) ;
#7901=DIRECTION ( 'NONE',  ( -0.000000000000000000, 1.000000000000000000, 1.877893248421448789E-16 ) ) ;
#7981=CARTESIAN_POINT ( 'NONE',  ( 0.01688885742776972607, -7.321065037175430668, -3.319543390096033164 ) ) ;
#7990=DIRECTION ( 'NONE',  ( 1.000000000000000000, 0.000000000000000000, 0.000000000000000000 ) ) ;
#8101=ORIENTED_EDGE ( 'NONE', *, *, #24848, .F. ) ;
#8131=ADVANCED_FACE ( 'NONE', ( #55605 ), #2156, .F. ) ;
#8149=ORIENTED_EDGE ( 'NONE', *, *, #27974, .T. ) ;
#8243=DIRECTION ( 'NONE',  ( 0.000000000000000000, 0.000000000000000000, -1.000000000000000000 ) ) ;
#8319=DIRECTION ( 'NONE',  ( 1.000000000000000000, 0.000000000000000000, 0.000000000000000000 ) ) ;
#8427=EDGE_LOOP ( 'NONE', ( #22555, #1702, #1669, #39294 ) ) ;
#8522=EDGE_LOOP ( 'NONE', ( #15796, #2759, #58518 ) ) ;
#8528=ORIENTED_EDGE ( 'NONE', *, *, #48317, .F. ) ;
#8707=ORIENTED_EDGE ( 'NONE', *, *, #13270, .T. ) ;
#8730=PRODUCT_DEFINITION ( 'UNKNOWN', '', #39993, #38055 ) ;
#8767=EDGE_CURVE ( 'NONE', #66603, #36977, #23182, .T. ) ;
#8869=LINE ( 'NONE', #24002, #26390 ) ;
#8872=VERTEX_POINT ( 'NONE', #6735 ) ;
#8877=EDGE_CURVE ( 'NONE', #54100, #15138, #40142, .T. ) ;
#8920=EDGE_CURVE ( 'NONE', #29802, #46252, #28182, .T. ) ;
#9146=PLANE ( 'NONE',  #57921 ) ;
#9270=CARTESIAN_POINT ( 'NONE',  ( 51.39999999999999858, 0.000000000000000000, 0.000000000000000000 ) ) ;
#9394=ORIENTED_EDGE ( 'NONE', *, *, #56443, .F. ) ;
#9445=VERTEX_POINT ( 'NONE', #63974 ) ;
#9637=CARTESIAN_POINT ( 'NONE',  ( 0.01688885742776671806, 7.321065037175427115, 3.319543390096037605 ) ) ;
#9644=CARTESIAN_POINT ( 'NONE',  ( 0.000000000000000000, -6.928203230275503444, 4.000000000000010658 ) ) ;
#10148=ORIENTED_EDGE ( 'NONE', *, *, #12558, .F. ) ;
#10163=CARTESIAN_POINT ( 'NONE',  ( 0.000000000000000000, 0.000000000000000000, 0.000000000000000000 ) ) ;
#10203=CIRCLE ( 'NONE', #29298, 0.4000000000000001887 ) ;
#10302=CARTESIAN_POINT ( 'NONE',  ( 0.000000000000000000, 0.000000000000000000, 8.000000000000000000 ) ) ;
#10334=ADVANCED_FACE ( 'NONE', ( #66953 ), #19087, .T. ) ;
#10384=EDGE_LOOP ( 'NONE', ( #9394, #48068, #53579, #47165, #31204, #1851 ) ) ;
#10455=CARTESIAN_POINT ( 'NONE',  ( 5.799999999999999822, 1.502314598737159031E-15, -8.000000000000000000 ) ) ;
#10534=ORIENTED_EDGE ( 'NONE', *, *, #55997, .F. ) ;
#10946=AXIS2_PLACEMENT_3D ( 'NONE', #10163, #47109, #63301 ) ;
#10987=VECTOR ( 'NONE', #48855, 1000.000000000000000 ) ;
#11054=DIRECTION ( 'NONE',  ( 1.000000000000000000, 0.000000000000000000, -0.000000000000000000 ) ) ;
#11169=FACE_OUTER_BOUND ( 'NONE', #34042, .T. ) ;
#11183=DIRECTION ( 'NONE',  ( 0.000000000000000000, 0.000000000000000000, 1.000000000000000000 ) ) ;
#11303=CARTESIAN_POINT ( 'NONE',  ( 5.799999999999999822, 0.000000000000000000, 0.000000000000000000 ) ) ;
#11391=CARTESIAN_POINT ( 'NONE',  ( 0.000000000000000000, 0.000000000000000000, 0.000000000000000000 ) ) ;
#11450=DIRECTION ( 'NONE',  ( 0.000000000000000000, 0.000000000000000000, -1.000000000000000000 ) ) ;
#11469=ORIENTED_EDGE ( 'NONE', *, *, #24848, .T. ) ;
#11582=CARTESIAN_POINT ( 'NONE',  ( 4.993259224064100499E-16, 0.3912769055735416113, -8.000000000000000000 ) ) ;
#11616=CARTESIAN_POINT ( 'NONE',  ( 0.000000000000000000, -6.928203230275509661, -3.999999999999999112 ) ) ;
#11695=CARTESIAN_POINT ( 'NONE',  ( -4.606165167168883666E-15, -7.321656987762866997, 3.318518101603013193 ) ) ;
#11767=B_SPLINE_CURVE_WITH_KNOTS ( 'NONE', 3,
 ( #55032, #6854, #886, #44488, #12842, #60320 ),
 .UNSPECIFIED., .F., .F.,
 ( 4, 2, 4 ),
 ( 0.02753256083616404531, 0.02987018135583072859, 0.03220780187549741186 ),
 .UNSPECIFIED. ) ;
#11903=AXIS2_PLACEMENT_3D ( 'NONE', #1219, #44831, #1564 ) ;
#12366=DIRECTION ( 'NONE',  ( 0.000000000000000000, 0.000000000000000000, -1.000000000000000000 ) ) ;
#12426=CYLINDRICAL_SURFACE ( 'NONE', #26530, 8.000000000000000000 ) ;
#12431=CARTESIAN_POINT ( 'NONE',  ( 0.01688885742776587845, -6.535341423375587766, 4.680456609903974829 ) ) ;
#12487=CONICAL_SURFACE ( 'NONE', #51799, 4.171999999999999709, 0.7853981633974437271 ) ;
#12517=FACE_OUTER_BOUND ( 'NONE', #3484, .T. ) ;
#12530=CARTESIAN_POINT ( 'NONE',  ( 0.7145311798163274108, 9.237604307034018802, -2.124379920709345337E-16 ) ) ;
#12558=EDGE_CURVE ( 'NONE', #6777, #9445, #46317, .T. ) ;
#12598=ORIENTED_EDGE ( 'NONE', *, *, #14397, .T. ) ;
#12704=CARTESIAN_POINT ( 'NONE',  ( 51.39999999999999858, 0.000000000000000000, 4.171999999999999709 ) ) ;
#12781=DIRECTION ( 'NONE',  ( 0.000000000000000000, 0.000000000000000000, -1.000000000000000000 ) ) ;
#12842=CARTESIAN_POINT ( 'NONE',  ( 0.4973051450610691537, -3.866309095671421669, -8.000000000000001776 ) ) ;
#12923=CARTESIAN_POINT ( 'NONE',  ( 0.08224679563971618035, -7.710515798486367700, -2.644994884459106910 ) ) ;
#12961=EDGE_CURVE ( 'NONE', #28268, #20719, #62643, .T. ) ;
#12966=ORIENTED_EDGE ( 'NONE', *, *, #56443, .T. ) ;
#12969=LINE ( 'NONE', #34432, #30403 ) ;
#13061=CARTESIAN_POINT ( 'NONE',  ( 6.400000000000000355, 4.618802153517001408, -8.000000000000000000 ) ) ;
#13071=DIRECTION ( 'NONE',  ( 0.000000000000000000, 0.000000000000000000, 1.000000000000000000 ) ) ;
#13226=VERTEX_POINT ( 'NONE', #41417 ) ;
#13270=EDGE_CURVE ( 'NONE', #30847, #66603, #26851, .T. ) ;
#13279=PLANE ( 'NONE',  #57569 ) ;
#13339=ORIENTED_EDGE ( 'NONE', *, *, #18344, .T. ) ;
#13346=SHAPE_REPRESENTATION_RELATIONSHIP ( 'NONE' , 'NONE' ,  #35767, #25672 ) ;
#13409=DIRECTION ( 'NONE',  ( -1.000000000000000000, -0.000000000000000000, -0.000000000000000000 ) ) ;
#13651=ORIENTED_EDGE ( 'NONE', *, *, #29773, .F. ) ;
#13998=CARTESIAN_POINT ( 'NONE',  ( 0.4969600502617471105, 4.995646404165273502, -7.347286611336972584 ) ) ;
#14050=EDGE_CURVE ( 'NONE', #28268, #27257, #59622, .T. ) ;
#14279=TOROIDAL_SURFACE ( 'NONE', #47940, 5.400000000000001243, 0.4000000000000000222 ) ;
#14292=EDGE_CURVE ( 'NONE', #24611, #28268, #42812, .T. ) ;
#14397=EDGE_CURVE ( 'NONE', #13226, #23841, #58417, .T. ) ;
#14405=ORIENTED_EDGE ( 'NONE', *, *, #18927, .F. ) ;
#14425=FACE_OUTER_BOUND ( 'NONE', #44279, .T. ) ;
#14496=DIRECTION ( 'NONE',  ( 1.000000000000000000, 0.000000000000000000, -0.000000000000000000 ) ) ;
#14532=ADVANCED_FACE ( 'NONE', ( #43048 ), #32854, .F. ) ;
#14792=SURFACE_STYLE_FILL_AREA ( #62650 ) ;
#15074=CARTESIAN_POINT ( 'NONE',  ( 6.800000000000000711, 0.000000000000000000, -5.400000000000001243 ) ) ;
#15138=VERTEX_POINT ( 'NONE', #946 ) ;
#15145=( LENGTH_UNIT ( ) NAMED_UNIT ( * ) SI_UNIT ( .MILLI., .METRE. ) );
#15341=VECTOR ( 'NONE', #13409, 1000.000000000000000 ) ;
#15599=CARTESIAN_POINT ( 'NONE',  ( 0.4988340113715861723, 3.871605243926953044, 7.999999999999998224 ) ) ;
#15669=ORIENTED_EDGE ( 'NONE', *, *, #14397, .F. ) ;
#15670=DIRECTION ( 'NONE',  ( 0.000000000000000000, 0.000000000000000000, 1.000000000000000000 ) ) ;
#15677=ORIENTED_EDGE ( 'NONE', *, *, #18261, .T. ) ;
#15796=ORIENTED_EDGE ( 'NONE', *, *, #12558, .T. ) ;
#15851=ORIENTED_EDGE ( 'NONE', *, *, #18261, .F. ) ;
#15926=CARTESIAN_POINT ( 'NONE',  ( 6.800000000000000711, 0.000000000000000000, 0.000000000000000000 ) ) ;
#15997=DIRECTION ( 'NONE',  ( -0.000000000000000000, 0.000000000000000000, -1.000000000000000000 ) ) ;
#16133=B_SPLINE_CURVE_WITH_KNOTS ( 'NONE', 3,
 ( #39172, #21578, #12431, #61989, #1890, #24379, #56035, #57074 ),
 .UNSPECIFIED., .F., .F.,
 ( 4, 2, 2, 4 ),
 ( 0.004673709593152172194, 0.005837709341827659014, 0.007001709090503144967, 0.009329708587854116872 ),
 .UNSPECIFIED. ) ;
#16204=CARTESIAN_POINT ( 'NONE',  ( 5.799999999999999822, -6.928203230275504332, 4.000000000000010658 ) ) ;
#16283=DIRECTION ( 'NONE',  ( 0.000000000000000000, 0.000000000000000000, -1.000000000000000000 ) ) ;
#16329=DIRECTION ( 'NONE',  ( 0.000000000000000000, 0.8660254037844379305, -0.5000000000000013323 ) ) ;
#16430=ORIENTED_EDGE ( 'NONE', *, *, #6934, .T. ) ;
#16501=DIRECTION ( 'NONE',  ( 0.000000000000000000, 0.000000000000000000, -1.000000000000000000 ) ) ;
#16555=CARTESIAN_POINT ( 'NONE',  ( 0.7145311798161616545, -4.618802153517262532, -8.000000000000001776 ) ) ;
#16600=ORIENTED_EDGE ( 'NONE', *, *, #30899, .T. ) ;
#16684=ADVANCED_FACE ( 'NONE', ( #30972 ), #52418, .T. ) ;
#16961=ADVANCED_FACE ( 'NONE', ( #23533 ), #40052, .F. ) ;
#16986=DIRECTION ( 'NONE',  ( -1.000000000000000000, -0.000000000000000000, -0.000000000000000000 ) ) ;
#17351=CARTESIAN_POINT ( 'NONE',  ( 5.799999999999999822, -4.618802153517012954, -8.000000000000001776 ) ) ;
#17398=EDGE_LOOP ( 'NONE', ( #68463, #64651, #6878, #41873 ) ) ;
#17470=FACE_OUTER_BOUND ( 'NONE', #1746, .T. ) ;
#17635=ORIENTED_EDGE ( 'NONE', *, *, #14292, .T. ) ;
#17685=CARTESIAN_POINT ( 'NONE',  ( 0.7145311798163268557, -9.237604307034018802, 5.946466066724412554E-16 ) ) ;
#17690=MANIFOLD_SOLID_BREP ( 'HeadFillet', #55266 ) ;
#17954=VECTOR ( 'NONE', #45044, 1000.000000000000000 ) ;
#18031=DIRECTION ( 'NONE',  ( 1.000000000000000000, 0.000000000000000000, 0.000000000000000000 ) ) ;
#18043=ORIENTED_EDGE ( 'NONE', *, *, #41689, .T. ) ;
#18052=ORIENTED_EDGE ( 'NONE', *, *, #29527, .F. ) ;
#18107=VECTOR ( 'NONE', #53554, 1000.000000000000000 ) ;
#18120=ORIENTED_EDGE ( 'NONE', *, *, #50893, .T. ) ;
#18243=CARTESIAN_POINT ( 'NONE',  ( 6.400000000000000355, 4.618802153517004960, 7.999999999999998224 ) ) ;
#18261=EDGE_CURVE ( 'NONE', #23841, #30847, #2349, .T. ) ;
#18267=EDGE_CURVE ( 'NONE', #38316, #40305, #10203, .T. ) ;
#18344=EDGE_CURVE ( 'NONE', #55226, #27257, #68542, .T. ) ;
#18450=DIRECTION ( 'NONE',  ( 1.000000000000000000, 0.000000000000000000, 0.000000000000000000 ) ) ;
#18480=CARTESIAN_POINT ( 'NONE',  ( 5.799999999999999822, 4.618802153517001408, -8.000000000000000000 ) ) ;
#18705=DIRECTION ( 'NONE',  ( -1.000000000000000000, -0.000000000000000000, -0.000000000000000000 ) ) ;
#18720=EDGE_LOOP ( 'NONE', ( #36740, #1967, #18043, #22516, #63748, #15851 ) ) ;
#18734=DIRECTION ( 'NONE',  ( 0.000000000000000000, -1.000000000000000000, 0.000000000000000000 ) ) ;
#18748=DIRECTION ( 'NONE',  ( 1.000000000000000000, 0.000000000000000000, 0.000000000000000000 ) ) ;
#18911=EDGE_CURVE ( 'NONE', #69105, #40305, #109, .T. ) ;
#18927=EDGE_CURVE ( 'NONE', #46252, #21223, #31430, .T. ) ;
#18928=EDGE_CURVE ( 'NONE', #20719, #24611, #57458, .T. ) ;
#19087=PLANE ( 'NONE',  #34545 ) ;
#19284=CARTESIAN_POINT ( 'NONE',  ( 0.000000000000000000, 9.237604307034018802, 1.301042606982603546E-15 ) ) ;
#19309=DIRECTION ( 'NONE',  ( -1.000000000000000000, -0.000000000000000000, -0.000000000000000000 ) ) ;
#19310=COLOUR_RGB ( '',0.7921568627450980005, 0.8196078431372548767, 0.9333333333333333481 ) ;
#19513=DIRECTION ( 'NONE',  ( -1.000000000000000000, -0.000000000000000000, -0.000000000000000000 ) ) ;
#19607=DIRECTION ( 'NONE',  ( 0.000000000000000000, 0.000000000000000000, 1.000000000000000000 ) ) ;
#19614=CARTESIAN_POINT ( 'NONE',  ( 0.7145311798163216377, 4.618802153517004960, 7.999999999999998224 ) ) ;
#19659=CARTESIAN_POINT ( 'NONE',  ( 6.400000000000000355, 4.618802153517001408, -8.000000000000000000 ) ) ;
#20015=DIRECTION ( 'NONE',  ( 0.000000000000000000, 0.000000000000000000, 1.000000000000000000 ) ) ;
#20034=ORIENTED_EDGE ( 'NONE', *, *, #57181, .F. ) ;
#20325=ORIENTED_EDGE ( 'NONE', *, *, #31005, .T. ) ;
#20368=EDGE_LOOP ( 'NONE', ( #51086, #8149, #47190 ) ) ;
#20372=LINE ( 'NONE', #53058, #21885 ) ;
#20409=CIRCLE ( 'NONE', #59705, 8.000000000000000000 ) ;
#20449=AXIS2_PLACEMENT_3D ( 'NONE', #21067, #5223, #43187 ) ;
#20493=UNCERTAINTY_MEASURE_WITH_UNIT (LENGTH_MEASURE( 1.000000000000000082E-05 ), #46034, 'distance_accuracy_value', 'NONE');
#20505=FACE_OUTER_BOUND ( 'NONE', #8522, .T. ) ;
#20614=EDGE_LOOP ( 'NONE', ( #36570, #12598, #64745 ) ) ;
#20719=VERTEX_POINT ( 'NONE', #62620 ) ;
#20762=FILL_AREA_STYLE_COLOUR ( '', #19310 ) ;
#20792=EDGE_CURVE ( 'NONE', #48097, #8872, #64290, .T. ) ;
#20851=DIRECTION ( 'NONE',  ( -0.7071067811865507924, 8.659560562354892183E-17, -0.7071067811865441310 ) ) ;
#20869=CARTESIAN_POINT ( 'NONE',  ( 0.08224679563971343255, 7.710515798486365036, 2.644994884459111351 ) ) ;
#20896=AXIS2_PLACEMENT_3D ( 'NONE', #37604, #44267, #16501 ) ;
#20959=VERTEX_POINT ( 'NONE', #44253 ) ;
#21067=CARTESIAN_POINT ( 'NONE',  ( 0.000000000000000000, 0.000000000000000000, 0.000000000000000000 ) ) ;
#21153=AXIS2_PLACEMENT_3D ( 'NONE', #33630, #54352, #6178 ) ;
#21223=VERTEX_POINT ( 'NONE', #19614 ) ;
#21395=CARTESIAN_POINT ( 'NONE',  ( 51.39999999999999858, 0.000000000000000000, 0.000000000000000000 ) ) ;
#21550=CARTESIAN_POINT ( 'NONE',  ( 6.400000000000000355, 0.000000000000000000, 0.000000000000000000 ) ) ;
#21578=CARTESIAN_POINT ( 'NONE',  ( -4.707385604365774134E-15, -6.732211846623389562, 4.339467034331192963 ) ) ;
#21665=ORIENTED_EDGE ( 'NONE', *, *, #61914, .T. ) ;
#21675=ORIENTED_EDGE ( 'NONE', *, *, #62911, .F. ) ;
#21701=ORIENTED_EDGE ( 'NONE', *, *, #14050, .T. ) ;
#21707=DIRECTION ( 'NONE',  ( 1.000000000000000000, 0.000000000000000000, -0.000000000000000000 ) ) ;
#21718=ORIENTED_EDGE ( 'NONE', *, *, #55175, .T. ) ;
#21794=CARTESIAN_POINT ( 'NONE',  ( 0.1317522424410015880, 1.959574484677831130, -8.000000000000001776 ) ) ;
#21800=VECTOR ( 'NONE', #65079, 1000.000000000000000 ) ;
#21807=DIRECTION ( 'NONE',  ( 0.000000000000000000, 0.000000000000000000, 1.000000000000000000 ) ) ;
#21885=VECTOR ( 'NONE', #5574, 1000.000000000000000 ) ;
#21966=PLANE ( 'NONE',  #58946 ) ;
#22115=CARTESIAN_POINT ( 'NONE',  ( 0.000000000000000000, 0.000000000000000000, 0.000000000000000000 ) ) ;
#22197=VECTOR ( 'NONE', #18734, 1000.000000000000000 ) ;
#22516=ORIENTED_EDGE ( 'NONE', *, *, #8767, .F. ) ;
#22518=ORIENTED_EDGE ( 'NONE', *, *, #41689, .F. ) ;
#22526=EDGE_CURVE ( 'NONE', #62198, #9445, #25192, .T. ) ;
#22555=ORIENTED_EDGE ( 'NONE', *, *, #39885, .T. ) ;
#22567=VECTOR ( 'NONE', #19309, 1000.000000000000000 ) ;
#22571=ORIENTED_EDGE ( 'NONE', *, *, #27974, .F. ) ;
#22635=CYLINDRICAL_SURFACE ( 'NONE', #32110, 5.000000000000000888 ) ;
#22724=ORIENTED_EDGE ( 'NONE', *, *, #61822, .F. ) ;
#22751=ORIENTED_EDGE ( 'NONE', *, *, #49528, .T. ) ;
#22826=CARTESIAN_POINT ( 'NONE',  ( 0.000000000000000000, 0.000000000000000000, 0.000000000000000000 ) ) ;
#22882=CARTESIAN_POINT ( 'NONE',  ( 0.4964154566687637438, -4.996589667937442414, -7.345652830558661250 ) ) ;
#22958=CARTESIAN_POINT ( 'NONE',  ( 0.06809871960542623892, -7.710219529346608702, 2.645508037661882916 ) ) ;
#23030=CIRCLE ( 'NONE', #28656, 0.4000000000000001887 ) ;
#23182=CIRCLE ( 'NONE', #40046, 8.000000000000000000 ) ;
#23245=CARTESIAN_POINT ( 'NONE',  ( 0.06809871960542558667, -6.146186931204439041, -5.354491962338080668 ) ) ;
#23503=AXIS2_PLACEMENT_3D ( 'NONE', #41758, #63215, #19607 ) ;
#23533=FACE_OUTER_BOUND ( 'NONE', #67799, .T. ) ;
#23841=VERTEX_POINT ( 'NONE', #10455 ) ;
#23938=CARTESIAN_POINT ( 'NONE',  ( 5.799999999999999822, 8.000000000000000000, 0.000000000000000000 ) ) ;
#24002=CARTESIAN_POINT ( 'NONE',  ( 6.400000000000000355, 9.237604307034018802, 0.000000000000000000 ) ) ;
#24074=ADVANCED_FACE ( 'NONE', ( #31836, #38144 ), #21966, .T. ) ;
#24088=CIRCLE ( 'NONE', #6076, 5.000000000000000888 ) ;
#24139=AXIS2_PLACEMENT_3D ( 'NONE', #62508, #30157, #52287 ) ;
#24166=DIRECTION ( 'NONE',  ( 0.000000000000000000, -0.8660254037844382635, -0.5000000000000008882 ) ) ;
#24379=CARTESIAN_POINT ( 'NONE',  ( 0.3173508448886507294, -5.375634714784613521, 6.689127551062007626 ) ) ;
#24406=EDGE_LOOP ( 'NONE', ( #56399, #47709, #2848 ) ) ;
#24439=ORIENTED_EDGE ( 'NONE', *, *, #18267, .F. ) ;
#24482=VECTOR ( 'NONE', #7901, 1000.000000000000000 ) ;
#24518=DIRECTION ( 'NONE',  ( 0.000000000000000000, 0.5000000000000007772, -0.8660254037844381525 ) ) ;
#24611=VERTEX_POINT ( 'NONE', #43510 ) ;
#24668=EDGE_LOOP ( 'NONE', ( #26070, #42904, #34354, #22571, #35706, #63780 ) ) ;
#24673=DIRECTION ( 'NONE',  ( 0.000000000000000000, 0.000000000000000000, 1.000000000000000000 ) ) ;
#24723=AXIS2_PLACEMENT_3D ( 'NONE', #802, #33857, #55298 ) ;
#24815=ORIENTED_EDGE ( 'NONE', *, *, #53762, .F. ) ;
#24848=EDGE_CURVE ( 'NONE', #8872, #48097, #47757, .T. ) ;
#24951=STYLED_ITEM ( 'NONE', ( #35913 ), #17690 ) ;
#25105=ADVANCED_FACE ( 'NONE', ( #34979 ), #51160, .T. ) ;
#25150=CARTESIAN_POINT ( 'NONE',  ( -1.007969207232617206E-15, -0.7818963812180719231, 7.999999999999996447 ) ) ;
#25192=CIRCLE ( 'NONE', #34181, 8.000000000000000000 ) ;
#25208=CARTESIAN_POINT ( 'NONE',  ( 50.57199999999998852, 0.000000000000000000, 0.000000000000000000 ) ) ;
#25467=DIRECTION ( 'NONE',  ( 0.000000000000000000, 0.000000000000000000, 1.000000000000000000 ) ) ;
#25616=DIRECTION ( 'NONE',  ( -0.7071067811865507924, 0.000000000000000000, 0.7071067811865441310 ) ) ;
#25672=ADVANCED_BREP_SHAPE_REPRESENTATION ( '', ( #17690, #66832 ), #28752 ) ;
#26070=ORIENTED_EDGE ( 'NONE', *, *, #52935, .F. ) ;
#26152=CARTESIAN_POINT ( 'NONE',  ( 0.08285530295198713369, 1.570896314769989255, 7.999999999999998224 ) ) ;
#26252=LINE ( 'NONE', #37483, #4983 ) ;
#26390=VECTOR ( 'NONE', #35245, 1000.000000000000000 ) ;
#26402=CARTESIAN_POINT ( 'NONE',  ( 0.000000000000000000, 1.502314598737159031E-15, -8.000000000000000000 ) ) ;
#26530=AXIS2_PLACEMENT_3D ( 'NONE', #6451, #16986, #44783 ) ;
#26534=CARTESIAN_POINT ( 'NONE',  ( 0.7145311798163198613, -4.618802153516998743, 7.999999999999998224 ) ) ;
#26649=CARTESIAN_POINT ( 'NONE',  ( 5.799999999999999822, 6.928203230275505220, 4.000000000000006217 ) ) ;
#26751=DIRECTION ( 'NONE',  ( 0.000000000000000000, -0.5000000000000013323, -0.8660254037844379305 ) ) ;
#26841=CARTESIAN_POINT ( 'NONE',  ( 0.4969600502617519400, 8.860760056385744932, 0.6527133886630308579 ) ) ;
#26851=CIRCLE ( 'NONE', #23503, 8.000000000000000000 ) ;
#27134=ORIENTED_EDGE ( 'NONE', *, *, #39308, .F. ) ;
#27257=VERTEX_POINT ( 'NONE', #47287 ) ;
#27404=ORIENTED_EDGE ( 'NONE', *, *, #68661, .F. ) ;
#27428=EDGE_LOOP ( 'NONE', ( #44043, #27846 ) ) ;
#27572=FACE_OUTER_BOUND ( 'NONE', #5799, .T. ) ;
#27603=ORIENTED_EDGE ( 'NONE', *, *, #8920, .T. ) ;
#27735=DIRECTION ( 'NONE',  ( -1.000000000000000000, -0.000000000000000000, -0.000000000000000000 ) ) ;
#27786=LINE ( 'NONE', #5293, #61513 ) ;
#27846=ORIENTED_EDGE ( 'NONE', *, *, #18911, .T. ) ;
#27970=ADVANCED_FACE ( 'NONE', ( #53771 ), #39984, .T. ) ;
#27974=EDGE_CURVE ( 'NONE', #20959, #62198, #31001, .T. ) ;
#27980=LINE ( 'NONE', #18480, #622 ) ;
#28100=VERTEX_POINT ( 'NONE', #34087 ) ;
#28182=LINE ( 'NONE', #61251, #36689 ) ;
#28268=VERTEX_POINT ( 'NONE', #4827 ) ;
#28350=CARTESIAN_POINT ( 'NONE',  ( 0.000000000000000000, 6.928203230275506108, 4.000000000000007105 ) ) ;
#28382=PRODUCT_CONTEXT ( 'NONE', #61055, 'mechanical' ) ;
#28452=CONICAL_SURFACE ( 'NONE', #1485, 8.000000000000000000, 1.047197551196600296 ) ;
#28481=ORIENTED_EDGE ( 'NONE', *, *, #47513, .T. ) ;
#28486=CARTESIAN_POINT ( 'NONE',  ( 5.799999999999999822, 4.618802153517001408, -8.000000000000000000 ) ) ;
#28656=AXIS2_PLACEMENT_3D ( 'NONE', #40282, #65989, #61725 ) ;
#28705=CIRCLE ( 'NONE', #5086, 8.000000000000000000 ) ;
#28752=( GEOMETRIC_REPRESENTATION_CONTEXT ( 3 ) GLOBAL_UNCERTAINTY_ASSIGNED_CONTEXT ( ( #20493 ) ) GLOBAL_UNIT_ASSIGNED_CONTEXT ( ( #46034, #34465, #35488 ) ) REPRESENTATION_CONTEXT ( 'NONE', 'WORKASPACE' ) );
#28873=B_SPLINE_CURVE_WITH_KNOTS ( 'NONE', 3,
 ( #31789, #4709, #51863, #36733, #25150, #62773 ),
 .UNSPECIFIED., .F., .F.,
 ( 4, 2, 4 ),
 ( 0.008690415895085790154, 0.01102883710845593661, 0.01336725832182608306 ),
 .UNSPECIFIED. ) ;
#28919=CARTESIAN_POINT ( 'NONE',  ( 0.000000000000000000, 0.000000000000000000, 8.000000000000000000 ) ) ;
#29061=ORIENTED_EDGE ( 'NONE', *, *, #18344, .F. ) ;
#29130=ORIENTED_EDGE ( 'NONE', *, *, #42961, .T. ) ;
#29298=AXIS2_PLACEMENT_3D ( 'NONE', #15074, #57300, #46735 ) ;
#29312=ADVANCED_FACE ( 'NONE', ( #17470 ), #14279, .F. ) ;
#29432=CARTESIAN_POINT ( 'NONE',  ( 0.3173508448886565581, -8.480771745766405800, -1.310872448937993928 ) ) ;
#29527=EDGE_CURVE ( 'NONE', #2227, #43392, #39292, .T. ) ;
#29542=VECTOR ( 'NONE', #20851, 1000.000000000000114 ) ;
#29688=CIRCLE ( 'NONE', #38673, 5.000000000000000888 ) ;
#29756=CARTESIAN_POINT ( 'NONE',  ( 6.400000000000000355, 0.000000000000000000, -5.400000000000001243 ) ) ;
#29773=EDGE_CURVE ( 'NONE', #33133, #29802, #67495, .T. ) ;
#29802=VERTEX_POINT ( 'NONE', #26649 ) ;
#29946=ORIENTED_EDGE ( 'NONE', *, *, #55997, .T. ) ;
#30135=CARTESIAN_POINT ( 'NONE',  ( 6.400000000000000355, 0.000000000000000000, 0.000000000000000000 ) ) ;
#30157=DIRECTION ( 'NONE',  ( 1.000000000000000000, 0.000000000000000000, 0.000000000000000000 ) ) ;
#30227=B_SPLINE_CURVE_WITH_KNOTS ( 'NONE', 3,
 ( #10302, #64466, #31095, #26152, #57818, #63441, #15599, #31771 ),
 .UNSPECIFIED., .F., .F.,
 ( 4, 2, 2, 4 ),
 ( 0.01336725832182608306, 0.01453745201803765055, 0.01570764571424921457, 0.01804803310667234956 ),
 .UNSPECIFIED. ) ;
#30360=VECTOR ( 'NONE', #54096, 1000.000000000000114 ) ;
#30403=VECTOR ( 'NONE', #55875, 1000.000000000000114 ) ;
#30442=DIRECTION ( 'NONE',  ( -1.000000000000000000, -0.000000000000000000, -0.000000000000000000 ) ) ;
#30468=SHAPE_DEFINITION_REPRESENTATION ( #47266, #35767 ) ;
#30699=CARTESIAN_POINT ( 'NONE',  ( 0.7145311798163216377, 4.618802153517004960, 7.999999999999998224 ) ) ;
#30847=VERTEX_POINT ( 'NONE', #4172 ) ;
#30859=AXIS2_PLACEMENT_3D ( 'NONE', #19284, #68847, #47059 ) ;
#30899=EDGE_CURVE ( 'NONE', #58924, #23841, #66048, .T. ) ;
#30972=FACE_OUTER_BOUND ( 'NONE', #17398, .T. ) ;
#31001=CIRCLE ( 'NONE', #20896, 8.000000000000000000 ) ;
#31005=EDGE_CURVE ( 'NONE', #9445, #28100, #6526, .T. ) ;
#31095=CARTESIAN_POINT ( 'NONE',  ( 0.01678220609565910654, 0.7854258609844486649, 7.999999999999998224 ) ) ;
#31104=VECTOR ( 'NONE', #51662, 999.9999999999998863 ) ;
#31204=ORIENTED_EDGE ( 'NONE', *, *, #55175, .F. ) ;
#31274=ORIENTED_EDGE ( 'NONE', *, *, #18267, .T. ) ;
#31320=EDGE_CURVE ( 'NONE', #23841, #55226, #34651, .T. ) ;
#31430=LINE ( 'NONE', #64123, #18107 ) ;
#31470=ORIENTED_EDGE ( 'NONE', *, *, #62911, .T. ) ;
#31771=CARTESIAN_POINT ( 'NONE',  ( 0.7145311798163216377, 4.618802153517004960, 7.999999999999998224 ) ) ;
#31772=CARTESIAN_POINT ( 'NONE',  ( 0.3173508448886549482, 8.480771745766404024, 1.310872448937998813 ) ) ;
#31789=CARTESIAN_POINT ( 'NONE',  ( 0.7145311798163198613, -4.618802153516998743, 7.999999999999998224 ) ) ;
#31836=FACE_BOUND ( 'NONE', #27428, .T. ) ;
#31908=ADVANCED_FACE ( 'NONE', ( #11169 ), #31949, .F. ) ;
#31949=PLANE ( 'NONE',  #68355 ) ;
#31979=CARTESIAN_POINT ( 'NONE',  ( 6.400000000000000355, 0.000000000000000000, 0.000000000000000000 ) ) ;
#32110=AXIS2_PLACEMENT_3D ( 'NONE', #40211, #61659, #50418 ) ;
#32139=DIRECTION ( 'NONE',  ( 0.000000000000000000, 0.000000000000000000, 1.000000000000000000 ) ) ;
#32282=EDGE_LOOP ( 'NONE', ( #64179, #334, #31274, #3076 ) ) ;
#32378=CARTESIAN_POINT ( 'NONE',  ( 0.000000000000000000, 0.000000000000000000, 0.000000000000000000 ) ) ;
#32635=CARTESIAN_POINT ( 'NONE',  ( 51.39999999999999858, 0.000000000000000000, 0.000000000000000000 ) ) ;
#32643=ORIENTED_EDGE ( 'NONE', *, *, #52935, .T. ) ;
#32681=DIRECTION ( 'NONE',  ( 1.000000000000000000, 0.000000000000000000, 0.000000000000000000 ) ) ;
#32707=AXIS2_PLACEMENT_3D ( 'NONE', #21550, #63443, #16283 ) ;
#32854=PLANE ( 'NONE',  #48306 ) ;
#33014=DIRECTION ( 'NONE',  ( 1.000000000000000000, 0.000000000000000000, -0.000000000000000000 ) ) ;
#33133=VERTEX_POINT ( 'NONE', #4454 ) ;
#33169=CARTESIAN_POINT ( 'NONE',  ( 5.799999999999999822, 8.000000000000000000, 0.000000000000000000 ) ) ;
#33188=FACE_OUTER_BOUND ( 'NONE', #18720, .T. ) ;
#33213=AXIS2_PLACEMENT_3D ( 'NONE', #51899, #3709, #68097 ) ;
#33328=CARTESIAN_POINT ( 'NONE',  ( 6.800000000000000711, 0.000000000000000000, 0.000000000000000000 ) ) ;
#33473=CARTESIAN_POINT ( 'NONE',  ( 5.799999999999999822, 4.618802153517004960, 7.999999999999998224 ) ) ;
#33630=CARTESIAN_POINT ( 'NONE',  ( 6.400000000000000355, -4.618802153517012954, -8.000000000000001776 ) ) ;
#33645=CARTESIAN_POINT ( 'NONE',  ( 0.4964154566687890013, 4.996589667937373136, 7.345652830558761615 ) ) ;
#33822=CARTESIAN_POINT ( 'NONE',  ( 0.000000000000000000, 0.000000000000000000, 5.000000000000000888 ) ) ;
#33857=DIRECTION ( 'NONE',  ( 1.000000000000000000, 0.000000000000000000, -0.000000000000000000 ) ) ;
#33866=AXIS2_PLACEMENT_3D ( 'NONE', #25208, #68115, #15670 ) ;
#33924=DIRECTION ( 'NONE',  ( 1.000000000000000000, 0.000000000000000000, 0.000000000000000000 ) ) ;
#33971=AXIS2_PLACEMENT_3D ( 'NONE', #31979, #33014, #49167 ) ;
#33998=CARTESIAN_POINT ( 'NONE',  ( 51.39999999999999858, 5.616230220889761452E-16, -4.171999999999999709 ) ) ;
#34042=EDGE_LOOP ( 'NONE', ( #53893, #20034 ) ) ;
#34087=CARTESIAN_POINT ( 'NONE',  ( 0.7145311798163268557, -9.237604307034018802, 5.946466066724412554E-16 ) ) ;
#34181=AXIS2_PLACEMENT_3D ( 'NONE', #11391, #11054, #53946 ) ;
#34301=EDGE_LOOP ( 'NONE', ( #68255, #11469 ) ) ;
#34336=CARTESIAN_POINT ( 'NONE',  ( 6.400000000000000355, 4.618802153517001408, -8.000000000000000000 ) ) ;
#34354=ORIENTED_EDGE ( 'NONE', *, *, #22526, .F. ) ;
#34432=CARTESIAN_POINT ( 'NONE',  ( 5.799999999999999822, -4.618802153517012954, -8.000000000000001776 ) ) ;
#34465=( NAMED_UNIT ( * ) PLANE_ANGLE_UNIT ( ) SI_UNIT ( $, .RADIAN. ) );
#34484=AXIS2_PLACEMENT_3D ( 'NONE', #67601, #51761, #67952 ) ;
#34545=AXIS2_PLACEMENT_3D ( 'NONE', #54980, #18748, #12781 ) ;
#34651=LINE ( 'NONE', #56086, #24482 ) ;
#34737=CARTESIAN_POINT ( 'NONE',  ( 5.799999999999999822, 8.000000000000000000, 0.000000000000000000 ) ) ;
#34884=EDGE_CURVE ( 'NONE', #46252, #36977, #49973, .T. ) ;
#34919=CARTESIAN_POINT ( 'NONE',  ( 5.799999999999999822, 4.618802153517004960, 7.999999999999998224 ) ) ;
#34979=FACE_OUTER_BOUND ( 'NONE', #20614, .T. ) ;
#35037=MECHANICAL_DESIGN_GEOMETRIC_PRESENTATION_REPRESENTATION('',(#24951),#57476);
#35059=CARTESIAN_POINT ( 'NONE',  ( -1.201657407838099433E-15, -7.124194613927628872, -3.660532965668815919 ) ) ;
#35119=EDGE_CURVE ( 'NONE', #55226, #13226, #62625, .T. ) ;
#35169=EDGE_CURVE ( 'NONE', #36960, #30847, #59045, .T. ) ;
#35204=CARTESIAN_POINT ( 'NONE',  ( 0.000000000000000000, 1.502314598737159031E-15, -8.000000000000000000 ) ) ;
#35245=DIRECTION ( 'NONE',  ( -1.000000000000000000, -0.000000000000000000, -0.000000000000000000 ) ) ;
#35256=EDGE_CURVE ( 'NONE', #30847, #58924, #12969, .T. ) ;
#35399=CARTESIAN_POINT ( 'NONE',  ( 6.400000000000000355, -4.618802153516998743, 7.999999999999998224 ) ) ;
#35402=PLANE ( 'NONE',  #38588 ) ;
#35488=( NAMED_UNIT ( * ) SI_UNIT ( $, .STERADIAN. ) SOLID_ANGLE_UNIT ( ) );
#35706=ORIENTED_EDGE ( 'NONE', *, *, #52436, .T. ) ;
#35760=CARTESIAN_POINT ( 'NONE',  ( 0.4969600502617522730, -8.860760056385746708, -0.6527133886630286375 ) ) ;
#35767=SHAPE_REPRESENTATION ( 'hex bolt gradeab_iso_ISO 4014 - M10 x 45 x 26-N', ( #66832 ), #28752 ) ;
#35913=PRESENTATION_STYLE_ASSIGNMENT (( #68605 ) ) ;
#36260=EDGE_LOOP ( 'NONE', ( #51737, #16600, #15677 ) ) ;
#36556=DIRECTION ( 'NONE',  ( 1.000000000000000000, 0.000000000000000000, 0.000000000000000000 ) ) ;
#36570=ORIENTED_EDGE ( 'NONE', *, *, #35119, .T. ) ;
#36604=( NAMED_UNIT ( * ) PLANE_ANGLE_UNIT ( ) SI_UNIT ( $, .RADIAN. ) );
#36623=AXIS2_PLACEMENT_3D ( 'NONE', #22826, #32681, #315 ) ;
#36628=CIRCLE ( 'NONE', #11903, 8.000000000000000000 ) ;
#36689=VECTOR ( 'NONE', #61597, 999.9999999999998863 ) ;
#36733=CARTESIAN_POINT ( 'NONE',  ( 0.06730325657896424341, -1.557442666625489025, 7.999999999999996447 ) ) ;
#36740=ORIENTED_EDGE ( 'NONE', *, *, #50893, .F. ) ;
#36787=EDGE_CURVE ( 'NONE', #27257, #46646, #55445, .T. ) ;
#36858=FACE_OUTER_BOUND ( 'NONE', #24668, .T. ) ;
#36933=DIRECTION ( 'NONE',  ( -1.000000000000000000, -0.000000000000000000, -0.000000000000000000 ) ) ;
#36960=VERTEX_POINT ( 'NONE', #6670 ) ;
#36977=VERTEX_POINT ( 'NONE', #50623 ) ;
#37017=EDGE_CURVE ( 'NONE', #54100, #57391, #67567, .T. ) ;
#37140=ORIENTED_EDGE ( 'NONE', *, *, #57409, .F. ) ;
#37148=CARTESIAN_POINT ( 'NONE',  ( 0.7145311798161616545, -4.618802153517262532, -8.000000000000001776 ) ) ;
#37246=CARTESIAN_POINT ( 'NONE',  ( 5.799999999999999822, -4.618802153517012954, -8.000000000000001776 ) ) ;
#37274=CONICAL_SURFACE ( 'NONE', #6958, 8.000000000000000000, 1.047197551196600296 ) ;
#37372=DIRECTION ( 'NONE',  ( 1.000000000000000000, 0.000000000000000000, -0.000000000000000000 ) ) ;
#37483=CARTESIAN_POINT ( 'NONE',  ( 5.799999999999999822, -9.237604307034018802, 3.355146209984123968E-17 ) ) ;
#37544=EDGE_CURVE ( 'NONE', #38316, #15138, #67612, .T. ) ;
#37604=CARTESIAN_POINT ( 'NONE',  ( 0.000000000000000000, 0.000000000000000000, 0.000000000000000000 ) ) ;
#37819=CIRCLE ( 'NONE', #34484, 5.400000000000001243 ) ;
#38011=CARTESIAN_POINT ( 'NONE',  ( -1.121471622164693649E-15, -6.534749472788167424, -4.681481898396976149 ) ) ;
#38016=ADVANCED_FACE ( 'NONE', ( #49226 ), #59091, .T. ) ;
#38055=PRODUCT_DEFINITION_CONTEXT ( 'detailed design', #64648, 'design' ) ;
#38067=DIRECTION ( 'NONE',  ( 0.000000000000000000, 0.000000000000000000, -1.000000000000000000 ) ) ;
#38144=FACE_OUTER_BOUND ( 'NONE', #34301, .T. ) ;
#38316=VERTEX_POINT ( 'NONE', #56604 ) ;
#38327=PRODUCT ( 'hex bolt gradeab_iso_ISO 4014 - M10 x 45 x 26-N', 'hex bolt gradeab_iso_ISO 4014 - M10 x 45 x 26-N', '', ( #28382 ) ) ;
#38421=DIRECTION ( 'NONE',  ( 0.000000000000000000, 0.000000000000000000, -1.000000000000000000 ) ) ;
#38436=FACE_OUTER_BOUND ( 'NONE', #1869, .T. ) ;
#38518=ADVANCED_FACE ( 'NONE', ( #40000 ), #13279, .T. ) ;
#38546=PLANE ( 'NONE',  #53312 ) ;
#38588=AXIS2_PLACEMENT_3D ( 'NONE', #3056, #24166, #24518 ) ;
#38673=AXIS2_PLACEMENT_3D ( 'NONE', #51870, #19513, #64753 ) ;
#38697=LINE ( 'NONE', #43952, #21800 ) ;
#39012=CARTESIAN_POINT ( 'NONE',  ( 51.39999999999999858, 0.000000000000000000, 0.000000000000000000 ) ) ;
#39100=ORIENTED_EDGE ( 'NONE', *, *, #57409, .T. ) ;
#39114=DIRECTION ( 'NONE',  ( 1.000000000000000000, 0.000000000000000000, -0.000000000000000000 ) ) ;
#39171=ORIENTED_EDGE ( 'NONE', *, *, #36787, .F. ) ;
#39172=CARTESIAN_POINT ( 'NONE',  ( 0.000000000000000000, -6.928203230275503444, 4.000000000000010658 ) ) ;
#39193=DIRECTION ( 'NONE',  ( 1.000000000000000000, 0.000000000000000000, 0.000000000000000000 ) ) ;
#39292=LINE ( 'NONE', #35399, #4131 ) ;
#39294=ORIENTED_EDGE ( 'NONE', *, *, #61914, .F. ) ;
#39308=EDGE_CURVE ( 'NONE', #21223, #20719, #63621, .T. ) ;
#39628=ORIENTED_EDGE ( 'NONE', *, *, #31320, .F. ) ;
#39704=DIRECTION ( 'NONE',  ( 0.000000000000000000, 0.000000000000000000, -1.000000000000000000 ) ) ;
#39840=CONICAL_SURFACE ( 'NONE', #24139, 8.000000000000000000, 1.047197551196600296 ) ;
#39841=LINE ( 'NONE', #34919, #22197 ) ;
#39885=EDGE_CURVE ( 'NONE', #43775, #68312, #3777, .T. ) ;
#39898=CIRCLE ( 'NONE', #61237, 4.171999999999999709 ) ;
#39944=DIRECTION ( 'NONE',  ( 0.000000000000000000, -1.000000000000000000, -1.877893248421448789E-16 ) ) ;
#39984=CONICAL_SURFACE ( 'NONE', #36623, 8.000000000000000000, 1.047197551196600296 ) ;
#39993=PRODUCT_DEFINITION_FORMATION_WITH_SPECIFIED_SOURCE ( 'ANY', '', #38327, .NOT_KNOWN. ) ;
#40000=FACE_OUTER_BOUND ( 'NONE', #53960, .T. ) ;
#40046=AXIS2_PLACEMENT_3D ( 'NONE', #11303, #50351, #13071 ) ;
#40052=PLANE ( 'NONE',  #57225 ) ;
#40142=LINE ( 'NONE', #33822, #15341 ) ;
#40211=CARTESIAN_POINT ( 'NONE',  ( 0.000000000000000000, 0.000000000000000000, 0.000000000000000000 ) ) ;
#40282=CARTESIAN_POINT ( 'NONE',  ( 6.800000000000000711, 6.613092715395708453E-16, 5.400000000000001243 ) ) ;
#40305=VERTEX_POINT ( 'NONE', #29756 ) ;
#40331=CARTESIAN_POINT ( 'NONE',  ( 0.000000000000000000, -6.928203230275509661, -3.999999999999999112 ) ) ;
#40390=LINE ( 'NONE', #46350, #53520 ) ;
#40552=CARTESIAN_POINT ( 'NONE',  ( 0.06809871960542752956, 6.146186931204407067, 5.354491962338127742 ) ) ;
#41078=CARTESIAN_POINT ( 'NONE',  ( 0.000000000000000000, 6.928203230275505220, -4.000000000000007994 ) ) ;
#41131=ORIENTED_EDGE ( 'NONE', *, *, #68661, .T. ) ;
#41259=CARTESIAN_POINT ( 'NONE',  ( -3.325451350920383131E-15, 6.534749472788146107, 4.681481898397001906 ) ) ;
#41264=CARTESIAN_POINT ( 'NONE',  ( 5.799999999999999822, 4.618802153517004960, 7.999999999999998224 ) ) ;
#41270=ORIENTED_EDGE ( 'NONE', *, *, #42961, .F. ) ;
#41417=CARTESIAN_POINT ( 'NONE',  ( 5.799999999999999822, 6.928203230275504332, -4.000000000000007994 ) ) ;
#41489=DIRECTION ( 'NONE',  ( 0.000000000000000000, 0.000000000000000000, -1.000000000000000000 ) ) ;
#41532=DIRECTION ( 'NONE',  ( -1.000000000000000000, -0.000000000000000000, -0.000000000000000000 ) ) ;
#41689=EDGE_CURVE ( 'NONE', #48097, #36977, #44744, .T. ) ;
#41758=CARTESIAN_POINT ( 'NONE',  ( 5.799999999999999822, 0.000000000000000000, 0.000000000000000000 ) ) ;
#41873=ORIENTED_EDGE ( 'NONE', *, *, #8877, .F. ) ;
#42328=CARTESIAN_POINT ( 'NONE',  ( 0.1306530452038101031, 7.903938623646867612, 2.309976723937613663 ) ) ;
#42429=VECTOR ( 'NONE', #6590, 1000.000000000000000 ) ;
#42812=B_SPLINE_CURVE_WITH_KNOTS ( 'NONE', 3,
 ( #12530, #55430, #51890, #62801, #3368, #57178 ),
 .UNSPECIFIED., .F., .F.,
 ( 4, 2, 4 ),
 ( 2.380731629581200700E-07, 0.002336973833157563775, 0.004673709593152168724 ),
 .UNSPECIFIED. ) ;
#42833=EDGE_CURVE ( 'NONE', #57391, #54100, #29688, .T. ) ;
#42904=ORIENTED_EDGE ( 'NONE', *, *, #7249, .F. ) ;
#42961=EDGE_CURVE ( 'NONE', #58924, #6777, #20372, .T. ) ;
#43048=FACE_OUTER_BOUND ( 'NONE', #10384, .T. ) ;
#43187=DIRECTION ( 'NONE',  ( 0.000000000000000000, 0.000000000000000000, -1.000000000000000000 ) ) ;
#43392=VERTEX_POINT ( 'NONE', #26534 ) ;
#43398=DIRECTION ( 'NONE',  ( 0.000000000000000000, 0.5000000000000013323, 0.8660254037844379305 ) ) ;
#43510=CARTESIAN_POINT ( 'NONE',  ( 0.7145311798163274108, 9.237604307034018802, -2.124379920709345337E-16 ) ) ;
#43752=CARTESIAN_POINT ( 'NONE',  ( 5.799999999999999822, 8.000000000000000000, 0.000000000000000000 ) ) ;
#43775=VERTEX_POINT ( 'NONE', #12704 ) ;
#43796=DIRECTION ( 'NONE',  ( -0.000000000000000000, 0.5000000000000009992, 0.8660254037844380415 ) ) ;
#43910=DIRECTION ( 'NONE',  ( -1.000000000000000000, -0.000000000000000000, -0.000000000000000000 ) ) ;
#43952=CARTESIAN_POINT ( 'NONE',  ( 6.400000000000000355, -9.237604307034018802, 3.355146209984123968E-17 ) ) ;
#44043=ORIENTED_EDGE ( 'NONE', *, *, #61822, .T. ) ;
#44100=FACE_OUTER_BOUND ( 'NONE', #55122, .T. ) ;
#44253=CARTESIAN_POINT ( 'NONE',  ( 0.000000000000000000, 0.000000000000000000, 8.000000000000000000 ) ) ;
#44267=DIRECTION ( 'NONE',  ( 1.000000000000000000, 0.000000000000000000, -0.000000000000000000 ) ) ;
#44279=EDGE_LOOP ( 'NONE', ( #39100, #51768, #3908 ) ) ;
#44488=CARTESIAN_POINT ( 'NONE',  ( 0.3157512944461042803, -3.097794232780332724, -8.000000000000001776 ) ) ;
#44558=DIRECTION ( 'NONE',  ( 0.000000000000000000, 0.000000000000000000, 1.000000000000000000 ) ) ;
#44668=CARTESIAN_POINT ( 'NONE',  ( 5.799999999999999822, 0.000000000000000000, 0.000000000000000000 ) ) ;
#44744=LINE ( 'NONE', #28919, #68937 ) ;
#44783=DIRECTION ( 'NONE',  ( 0.000000000000000000, 0.000000000000000000, 1.000000000000000000 ) ) ;
#44812=DIRECTION ( 'NONE',  ( 0.000000000000000000, 0.000000000000000000, -1.000000000000000000 ) ) ;
#44831=DIRECTION ( 'NONE',  ( -1.000000000000000000, -0.000000000000000000, -0.000000000000000000 ) ) ;
#44874=DIRECTION ( 'NONE',  ( 0.000000000000000000, -1.877893248421448789E-16, 1.000000000000000000 ) ) ;
#44919=ORIENTED_EDGE ( 'NONE', *, *, #30899, .F. ) ;
#44929=AXIS2_PLACEMENT_3D ( 'NONE', #47292, #30442, #3023 ) ;
#45044=DIRECTION ( 'NONE',  ( 0.000000000000000000, -1.000000000000000000, 0.000000000000000000 ) ) ;
#45477=FACE_OUTER_BOUND ( 'NONE', #51119, .T. ) ;
#45634=FACE_OUTER_BOUND ( 'NONE', #24406, .T. ) ;
#45683=EDGE_LOOP ( 'NONE', ( #21701, #67299, #32643 ) ) ;
#45799=CIRCLE ( 'NONE', #64876, 8.000000000000000000 ) ;
#46034=( LENGTH_UNIT ( ) NAMED_UNIT ( * ) SI_UNIT ( .MILLI., .METRE. ) );
#46252=VERTEX_POINT ( 'NONE', #41264 ) ;
#46317=B_SPLINE_CURVE_WITH_KNOTS ( 'NONE', 3,
 ( #16555, #22882, #65096, #23245, #38011, #11616 ),
 .UNSPECIFIED., .F., .F.,
 ( 4, 2, 4 ),
 ( 2.380731631042988191E-07, 0.002336973833157630128, 0.004673709593152156581 ),
 .UNSPECIFIED. ) ;
#46331=EDGE_LOOP ( 'NONE', ( #57098, #13339, #51780, #65627, #10534, #37140 ) ) ;
#46350=CARTESIAN_POINT ( 'NONE',  ( 51.39999999999999858, 0.000000000000000000, 4.171999999999999709 ) ) ;
#46541=CARTESIAN_POINT ( 'NONE',  ( 6.400000000000000355, 0.000000000000000000, 8.000000000000000000 ) ) ;
#46646=VERTEX_POINT ( 'NONE', #35204 ) ;
#46692=CARTESIAN_POINT ( 'NONE',  ( 0.7145311798163209716, 4.618802153517001408, -8.000000000000000000 ) ) ;
#46735=DIRECTION ( 'NONE',  ( 0.000000000000000000, 0.000000000000000000, -1.000000000000000000 ) ) ;
#46851=DIRECTION ( 'NONE',  ( 0.000000000000000000, 0.000000000000000000, -1.000000000000000000 ) ) ;
#46914=ORIENTED_EDGE ( 'NONE', *, *, #42833, .T. ) ;
#47059=DIRECTION ( 'NONE',  ( -0.000000000000000000, 0.000000000000000000, -1.000000000000000000 ) ) ;
#47109=DIRECTION ( 'NONE',  ( 1.000000000000000000, 0.000000000000000000, -0.000000000000000000 ) ) ;
#47165=ORIENTED_EDGE ( 'NONE', *, *, #55836, .F. ) ;
#47190=ORIENTED_EDGE ( 'NONE', *, *, #63698, .T. ) ;
#47230=LINE ( 'NONE', #69024, #29542 ) ;
#47266=PRODUCT_DEFINITION_SHAPE ( 'NONE', 'NONE',  #8730 ) ;
#47287=CARTESIAN_POINT ( 'NONE',  ( 0.7145311798163209716, 4.618802153517001408, -8.000000000000000000 ) ) ;
#47292=CARTESIAN_POINT ( 'NONE',  ( 5.799999999999999822, 0.000000000000000000, 0.000000000000000000 ) ) ;
#47371=CARTESIAN_POINT ( 'NONE',  ( 0.3173508448886513400, 5.375634714784618851, -6.689127551062007626 ) ) ;
#47389=PLANE ( 'NONE',  #30859 ) ;
#47407=ORIENTED_EDGE ( 'NONE', *, *, #22526, .T. ) ;
#47512=EDGE_LOOP ( 'NONE', ( #8101, #18120, #15669, #68417, #60968, #22518 ) ) ;
#47513=EDGE_CURVE ( 'NONE', #36977, #29802, #45799, .T. ) ;
#47709=ORIENTED_EDGE ( 'NONE', *, *, #39308, .T. ) ;
#47757=CIRCLE ( 'NONE', #7361, 8.000000000000000000 ) ;
#47811=ORIENTED_EDGE ( 'NONE', *, *, #18928, .T. ) ;
#47940=AXIS2_PLACEMENT_3D ( 'NONE', #33328, #21707, #1650 ) ;
#47998=CARTESIAN_POINT ( 'NONE',  ( 6.400000000000000355, 9.237604307034018802, 1.301042606982603546E-15 ) ) ;
#48018=EDGE_LOOP ( 'NONE', ( #24815, #57741, #21665, #49941 ) ) ;
#48030=ORIENTED_EDGE ( 'NONE', *, *, #35256, .F. ) ;
#48068=ORIENTED_EDGE ( 'NONE', *, *, #29527, .T. ) ;
#48097=VERTEX_POINT ( 'NONE', #46541 ) ;
#48119=CARTESIAN_POINT ( 'NONE',  ( 0.000000000000000000, 0.000000000000000000, 0.000000000000000000 ) ) ;
#48253=CARTESIAN_POINT ( 'NONE',  ( 0.000000000000000000, 0.000000000000000000, 0.000000000000000000 ) ) ;
#48268=CARTESIAN_POINT ( 'NONE',  ( 0.000000000000000000, 6.928203230275506108, 4.000000000000007105 ) ) ;
#48306=AXIS2_PLACEMENT_3D ( 'NONE', #143, #16329, #43398 ) ;
#48317=EDGE_CURVE ( 'NONE', #57391, #38316, #64027, .T. ) ;
#48446=DIRECTION ( 'NONE',  ( -1.000000000000000000, -0.000000000000000000, -0.000000000000000000 ) ) ;
#48489=CARTESIAN_POINT ( 'NONE',  ( 6.400000000000000355, 6.613092715395708453E-16, 5.400000000000001243 ) ) ;
#48593=DIRECTION ( 'NONE',  ( 1.000000000000000000, 0.000000000000000000, 0.000000000000000000 ) ) ;
#48609=ORIENTED_EDGE ( 'NONE', *, *, #8920, .F. ) ;
#48855=DIRECTION ( 'NONE',  ( -1.000000000000000000, -0.000000000000000000, -0.000000000000000000 ) ) ;
#49167=DIRECTION ( 'NONE',  ( 0.000000000000000000, 0.000000000000000000, -1.000000000000000000 ) ) ;
#49226=FACE_OUTER_BOUND ( 'NONE', #47512, .T. ) ;
#49267=DIRECTION ( 'NONE',  ( 0.000000000000000000, -0.5000000000000009992, -0.8660254037844380415 ) ) ;
#49528=EDGE_CURVE ( 'NONE', #66603, #36960, #27786, .T. ) ;
#49532=DIRECTION ( 'NONE',  ( 0.000000000000000000, 0.000000000000000000, 1.000000000000000000 ) ) ;
#49685=DIRECTION ( 'NONE',  ( -1.000000000000000000, -0.000000000000000000, -0.000000000000000000 ) ) ;
#49780=FACE_OUTER_BOUND ( 'NONE', #53747, .T. ) ;
#49941=ORIENTED_EDGE ( 'NONE', *, *, #42833, .F. ) ;
#49973=LINE ( 'NONE', #33473, #17954 ) ;
#49995=ORIENTED_EDGE ( 'NONE', *, *, #8767, .T. ) ;
#50035=CARTESIAN_POINT ( 'NONE',  ( 0.3167204509598373074, -8.479269695850863542, 1.313474075707214084 ) ) ;
#50080=AXIS2_PLACEMENT_3D ( 'NONE', #2971, #18450, #8243 ) ;
#50219=ORIENTED_EDGE ( 'NONE', *, *, #18927, .T. ) ;
#50351=DIRECTION ( 'NONE',  ( -1.000000000000000000, -0.000000000000000000, -0.000000000000000000 ) ) ;
#50418=DIRECTION ( 'NONE',  ( 0.000000000000000000, 0.000000000000000000, 1.000000000000000000 ) ) ;
#50530=CARTESIAN_POINT ( 'NONE',  ( 0.000000000000000000, 0.000000000000000000, 0.000000000000000000 ) ) ;
#50623=CARTESIAN_POINT ( 'NONE',  ( 5.799999999999999822, 0.000000000000000000, 8.000000000000000000 ) ) ;
#50729=AXIS2_PLACEMENT_3D ( 'NONE', #15926, #37372, #38421 ) ;
#50893=EDGE_CURVE ( 'NONE', #8872, #23841, #3001, .T. ) ;
#50897=AXIS2_PLACEMENT_3D ( 'NONE', #48253, #48593, #38067 ) ;
#50982=DIRECTION ( 'NONE',  ( -1.000000000000000000, -0.000000000000000000, -0.000000000000000000 ) ) ;
#51086=ORIENTED_EDGE ( 'NONE', *, *, #62806, .T. ) ;
#51089=ADVANCED_FACE ( 'NONE', ( #6085 ), #12487, .T. ) ;
#51119=EDGE_LOOP ( 'NONE', ( #8528, #46914, #7725, #41131 ) ) ;
#51160=PLANE ( 'NONE',  #50080 ) ;
#51662=DIRECTION ( 'NONE',  ( 0.000000000000000000, -0.5000000000000008882, 0.8660254037844382635 ) ) ;
#51737=ORIENTED_EDGE ( 'NONE', *, *, #35256, .T. ) ;
#51761=DIRECTION ( 'NONE',  ( -1.000000000000000000, -0.000000000000000000, 0.000000000000000000 ) ) ;
#51768=ORIENTED_EDGE ( 'NONE', *, *, #29773, .T. ) ;
#51780=ORIENTED_EDGE ( 'NONE', *, *, #14050, .F. ) ;
#51799=AXIS2_PLACEMENT_3D ( 'NONE', #58859, #49685, #32139 ) ;
#51863=CARTESIAN_POINT ( 'NONE',  ( 0.3157512944565053492, -3.097794232830064498, 7.999999999999998224 ) ) ;
#51870=CARTESIAN_POINT ( 'NONE',  ( 50.57199999999998852, 0.000000000000000000, 0.000000000000000000 ) ) ;
#51890=CARTESIAN_POINT ( 'NONE',  ( 0.3167204509598382511, 8.479269695850865318, -1.313474075707213418 ) ) ;
#51899=CARTESIAN_POINT ( 'NONE',  ( 0.000000000000000000, 0.000000000000000000, 0.000000000000000000 ) ) ;
#51918=ORIENTED_EDGE ( 'NONE', *, *, #34884, .T. ) ;
#52287=DIRECTION ( 'NONE',  ( 0.000000000000000000, 0.000000000000000000, -1.000000000000000000 ) ) ;
#52317=CARTESIAN_POINT ( 'NONE',  ( 0.08224679563971232232, 6.145890662064651622, -5.355005115540898863 ) ) ;
#52383=FACE_OUTER_BOUND ( 'NONE', #45683, .T. ) ;
#52418=CYLINDRICAL_SURFACE ( 'NONE', #57485, 5.000000000000000888 ) ;
#52429=CARTESIAN_POINT ( 'NONE',  ( 5.799999999999999822, 0.000000000000000000, 0.000000000000000000 ) ) ;
#52436=EDGE_CURVE ( 'NONE', #20959, #20719, #20409, .T. ) ;
#52882=VECTOR ( 'NONE', #67711, 1000.000000000000000 ) ;
#52935=EDGE_CURVE ( 'NONE', #46646, #28268, #5884, .T. ) ;
#53058=CARTESIAN_POINT ( 'NONE',  ( 6.400000000000000355, -4.618802153517012954, -8.000000000000001776 ) ) ;
#53204=CARTESIAN_POINT ( 'NONE',  ( -3.476223215531647803E-15, 7.124194613927619990, 3.660532965668822580 ) ) ;
#53312=AXIS2_PLACEMENT_3D ( 'NONE', #34336, #44874, #39944 ) ;
#53520=VECTOR ( 'NONE', #25616, 1000.000000000000114 ) ;
#53524=CARTESIAN_POINT ( 'NONE',  ( 5.799999999999999822, -4.618802153516998743, 7.999999999999998224 ) ) ;
#53554=DIRECTION ( 'NONE',  ( -1.000000000000000000, -0.000000000000000000, -0.000000000000000000 ) ) ;
#53579=ORIENTED_EDGE ( 'NONE', *, *, #63698, .F. ) ;
#53747=EDGE_LOOP ( 'NONE', ( #2709, #21718, #62414, #10148, #41270, #48030 ) ) ;
#53762=EDGE_CURVE ( 'NONE', #68312, #57391, #47230, .T. ) ;
#53771=FACE_OUTER_BOUND ( 'NONE', #1531, .T. ) ;
#53793=CARTESIAN_POINT ( 'NONE',  ( 0.4988340113754565208, 3.871605243940355656, -8.000000000000000000 ) ) ;
#53893=ORIENTED_EDGE ( 'NONE', *, *, #39885, .F. ) ;
#53946=DIRECTION ( 'NONE',  ( 0.000000000000000000, 0.000000000000000000, -1.000000000000000000 ) ) ;
#53960=EDGE_LOOP ( 'NONE', ( #31470, #12966, #49995 ) ) ;
#53999=PLANE ( 'NONE',  #21153 ) ;
#54096=DIRECTION ( 'NONE',  ( 0.000000000000000000, 0.4999999999999998890, -0.8660254037844387076 ) ) ;
#54100=VERTEX_POINT ( 'NONE', #610 ) ;
#54348=CARTESIAN_POINT ( 'NONE',  ( 50.57199999999998852, 6.123233995736767268E-16, -5.000000000000000888 ) ) ;
#54352=DIRECTION ( 'NONE',  ( -0.000000000000000000, 0.8660254037844387076, 0.4999999999999998890 ) ) ;
#54447=ADVANCED_FACE ( 'NONE', ( #61444 ), #35402, .F. ) ;
#54628=AXIS2_PLACEMENT_3D ( 'NONE', #9270, #3999, #25467 ) ;
#54660=DIRECTION ( 'NONE',  ( 0.000000000000000000, 0.000000000000000000, -1.000000000000000000 ) ) ;
#54980=CARTESIAN_POINT ( 'NONE',  ( 5.799999999999999822, 8.000000000000000000, 0.000000000000000000 ) ) ;
#55032=CARTESIAN_POINT ( 'NONE',  ( 0.000000000000000000, 1.502314598737159031E-15, -8.000000000000000000 ) ) ;
#55122=EDGE_LOOP ( 'NONE', ( #27603, #51918, #28481 ) ) ;
#55175=EDGE_CURVE ( 'NONE', #36960, #28100, #38697, .T. ) ;
#55226=VERTEX_POINT ( 'NONE', #28486 ) ;
#55266=CLOSED_SHELL ( 'NONE', ( #29312, #38016, #51089, #16684, #24074, #7818, #60592, #31908, #25105, #7491, #3037, #38518, #55772, #10334, #57949, #69266, #27970, #56239, #59449, #2068, #66892, #4071, #58734, #63502, #14532, #16961, #54447, #8131, #65341 ) ) ;
#55298=DIRECTION ( 'NONE',  ( 0.000000000000000000, 0.000000000000000000, -1.000000000000000000 ) ) ;
#55430=CARTESIAN_POINT ( 'NONE',  ( 0.4964154566687932202, 8.859816792613651515, -0.6543471694412406059 ) ) ;
#55445=B_SPLINE_CURVE_WITH_KNOTS ( 'NONE', 3,
 ( #58392, #53793, #5616, #21794, #339, #4935, #11582, #26402 ),
 .UNSPECIFIED., .F., .F.,
 ( 4, 2, 2, 4 ),
 ( 0.02285338878549945940, 0.02519297481083175236, 0.02636276782349789710, 0.02753256083616404531 ),
 .UNSPECIFIED. ) ;
#55465=CARTESIAN_POINT ( 'NONE',  ( 5.799999999999999822, 4.618802153517001408, -8.000000000000000000 ) ) ;
#55605=FACE_OUTER_BOUND ( 'NONE', #46331, .T. ) ;
#55646=CONICAL_SURFACE ( 'NONE', #33213, 8.000000000000000000, 1.047197551196600296 ) ;
#55657=CARTESIAN_POINT ( 'NONE',  ( 0.4964154566687932202, -8.859816792613647962, 0.6543471694412412720 ) ) ;
#55772=ADVANCED_FACE ( 'NONE', ( #38436 ), #59525, .T. ) ;
#55836=EDGE_CURVE ( 'NONE', #28100, #62198, #66261, .T. ) ;
#55875=DIRECTION ( 'NONE',  ( 0.000000000000000000, 0.4999999999999998890, -0.8660254037844387076 ) ) ;
#55997=EDGE_CURVE ( 'NONE', #33133, #24611, #8869, .T. ) ;
#56035=CARTESIAN_POINT ( 'NONE',  ( 0.4969600502617472215, -4.995646404165269949, 7.347286611336972584 ) ) ;
#56068=PLANE ( 'NONE',  #62087 ) ;
#56086=CARTESIAN_POINT ( 'NONE',  ( 5.799999999999999822, 4.618802153517001408, -8.000000000000000000 ) ) ;
#56239=ADVANCED_FACE ( 'NONE', ( #45634 ), #39840, .T. ) ;
#56399=ORIENTED_EDGE ( 'NONE', *, *, #65193, .T. ) ;
#56443=EDGE_CURVE ( 'NONE', #2227, #66603, #26252, .T. ) ;
#56519=DIRECTION ( 'NONE',  ( 0.000000000000000000, 0.000000000000000000, -1.000000000000000000 ) ) ;
#56573=DIRECTION ( 'NONE',  ( -1.000000000000000000, 0.000000000000000000, -0.000000000000000000 ) ) ;
#56604=CARTESIAN_POINT ( 'NONE',  ( 6.800000000000000711, 6.123233995736767268E-16, -5.000000000000000888 ) ) ;
#56668=AXIS2_PLACEMENT_3D ( 'NONE', #33169, #18031, #64826 ) ;
#56942=CARTESIAN_POINT ( 'NONE',  ( 5.799999999999999822, 9.237604307034018802, 0.000000000000000000 ) ) ;
#57074=CARTESIAN_POINT ( 'NONE',  ( 0.7145311798163198613, -4.618802153516998743, 7.999999999999998224 ) ) ;
#57098=ORIENTED_EDGE ( 'NONE', *, *, #35119, .F. ) ;
#57178=CARTESIAN_POINT ( 'NONE',  ( 0.000000000000000000, 6.928203230275505220, -4.000000000000007994 ) ) ;
#57181=EDGE_CURVE ( 'NONE', #68312, #43775, #39898, .T. ) ;
#57188=FACE_OUTER_BOUND ( 'NONE', #20368, .T. ) ;
#57225=AXIS2_PLACEMENT_3D ( 'NONE', #18243, #39704, #56573 ) ;
#57300=DIRECTION ( 'NONE',  ( 0.000000000000000000, -1.000000000000000000, 0.000000000000000000 ) ) ;
#57391=VERTEX_POINT ( 'NONE', #54348 ) ;
#57409=EDGE_CURVE ( 'NONE', #13226, #33133, #27980, .T. ) ;
#57458=B_SPLINE_CURVE_WITH_KNOTS ( 'NONE', 3,
 ( #48268, #53204, #9637, #20869, #42328, #31772, #26841, #4357 ),
 .UNSPECIFIED., .F., .F.,
 ( 4, 2, 2, 4 ),
 ( 0.004673709593152147908, 0.005837709341827639065, 0.007001709090503129354, 0.009329708587854111668 ),
 .UNSPECIFIED. ) ;
#57459=FACE_OUTER_BOUND ( 'NONE', #48018, .T. ) ;
#57476=( GEOMETRIC_REPRESENTATION_CONTEXT ( 3 ) GLOBAL_UNCERTAINTY_ASSIGNED_CONTEXT ( ( #57792 ) ) GLOBAL_UNIT_ASSIGNED_CONTEXT ( ( #15145, #36604, #58054 ) ) REPRESENTATION_CONTEXT ( 'NONE', 'WORKASPACE' ) );
#57485=AXIS2_PLACEMENT_3D ( 'NONE', #3886, #36933, #68924 ) ;
#57569=AXIS2_PLACEMENT_3D ( 'NONE', #34737, #7990, #56519 ) ;
#57689=DIRECTION ( 'NONE',  ( -0.000000000000000000, 0.5000000000000009992, 0.8660254037844380415 ) ) ;
#57741=ORIENTED_EDGE ( 'NONE', *, *, #57181, .T. ) ;
#57792=UNCERTAINTY_MEASURE_WITH_UNIT (LENGTH_MEASURE( 1.000000000000000082E-05 ), #15145, 'distance_accuracy_value', 'NONE');
#57818=CARTESIAN_POINT ( 'NONE',  ( 0.1317522424472098441, 1.959574484719855292, 7.999999999999998224 ) ) ;
#57921=AXIS2_PLACEMENT_3D ( 'NONE', #23938, #64589, #11450 ) ;
#57943=CARTESIAN_POINT ( 'NONE',  ( 0.01688885742776611437, 6.535341423375590431, -4.680456609903974829 ) ) ;
#57949=ADVANCED_FACE ( 'NONE', ( #33188 ), #12426, .T. ) ;
#58054=( NAMED_UNIT ( * ) SI_UNIT ( $, .STERADIAN. ) SOLID_ANGLE_UNIT ( ) );
#58233=DIRECTION ( 'NONE',  ( 1.000000000000000000, 0.000000000000000000, -0.000000000000000000 ) ) ;
#58279=CARTESIAN_POINT ( 'NONE',  ( -3.973643313806734888E-15, 6.732211846623391338, -4.339467034331192075 ) ) ;
#58392=CARTESIAN_POINT ( 'NONE',  ( 0.7145311798163209716, 4.618802153517001408, -8.000000000000000000 ) ) ;
#58417=CIRCLE ( 'NONE', #44929, 8.000000000000000000 ) ;
#58518=ORIENTED_EDGE ( 'NONE', *, *, #64959, .T. ) ;
#58644=AXIS2_PLACEMENT_3D ( 'NONE', #32378, #5970, #21807 ) ;
#58734=ADVANCED_FACE ( 'NONE', ( #12517 ), #38546, .F. ) ;
#58859=CARTESIAN_POINT ( 'NONE',  ( 51.39999999999999858, 0.000000000000000000, 0.000000000000000000 ) ) ;
#58924=VERTEX_POINT ( 'NONE', #17351 ) ;
#58946=AXIS2_PLACEMENT_3D ( 'NONE', #47998, #65231, #15997 ) ;
#59045=LINE ( 'NONE', #37246, #30360 ) ;
#59091=CYLINDRICAL_SURFACE ( 'NONE', #58644, 8.000000000000000000 ) ;
#59449=ADVANCED_FACE ( 'NONE', ( #57188 ), #55646, .T. ) ;
#59469=ORIENTED_EDGE ( 'NONE', *, *, #34884, .F. ) ;
#59525=PLANE ( 'NONE',  #56668 ) ;
#59622=B_SPLINE_CURVE_WITH_KNOTS ( 'NONE', 3,
 ( #41078, #58279, #57943, #52317, #4481, #47371, #13998, #46692 ),
 .UNSPECIFIED., .F., .F.,
 ( 4, 2, 2, 4 ),
 ( 0.004673709593152168724, 0.005837709341827655544, 0.007001709090503143232, 0.009329708587854116872 ),
 .UNSPECIFIED. ) ;
#59705=AXIS2_PLACEMENT_3D ( 'NONE', #22115, #27735, #305 ) ;
#60320=CARTESIAN_POINT ( 'NONE',  ( 0.7145311798161616545, -4.618802153517262532, -8.000000000000001776 ) ) ;
#60509=EDGE_CURVE ( 'NONE', #29802, #13226, #36628, .T. ) ;
#60538=DIRECTION ( 'NONE',  ( 0.000000000000000000, -0.8660254037844380415, 0.5000000000000009992 ) ) ;
#60592=ADVANCED_FACE ( 'NONE', ( #57459 ), #63640, .T. ) ;
#60681=VECTOR ( 'NONE', #57689, 1000.000000000000000 ) ;
#60968=ORIENTED_EDGE ( 'NONE', *, *, #47513, .F. ) ;
#61038=CARTESIAN_POINT ( 'NONE',  ( 0.000000000000000000, 9.797174393178825657E-16, -8.000000000000000000 ) ) ;
#61055=APPLICATION_CONTEXT ( 'automotive_design' ) ;
#61078=AXIS2_PLACEMENT_3D ( 'NONE', #39012, #43910, #49532 ) ;
#61237=AXIS2_PLACEMENT_3D ( 'NONE', #21395, #48446, #11183 ) ;
#61251=CARTESIAN_POINT ( 'NONE',  ( 5.799999999999999822, 9.237604307034018802, 0.000000000000000000 ) ) ;
#61279=ORIENTED_EDGE ( 'NONE', *, *, #64959, .F. ) ;
#61444=FACE_OUTER_BOUND ( 'NONE', #65089, .T. ) ;
#61513=VECTOR ( 'NONE', #26751, 1000.000000000000000 ) ;
#61597=DIRECTION ( 'NONE',  ( 0.000000000000000000, -0.5000000000000008882, 0.8660254037844382635 ) ) ;
#61659=DIRECTION ( 'NONE',  ( -1.000000000000000000, -0.000000000000000000, -0.000000000000000000 ) ) ;
#61725=DIRECTION ( 'NONE',  ( 0.000000000000000000, 1.224646799147353207E-16, 1.000000000000000000 ) ) ;
#61822=EDGE_CURVE ( 'NONE', #40305, #69105, #37819, .T. ) ;
#61914=EDGE_CURVE ( 'NONE', #43775, #54100, #40390, .T. ) ;
#61989=CARTESIAN_POINT ( 'NONE',  ( 0.08224679563971203089, -6.145890662064649845, 5.355005115540899752 ) ) ;
#62087=AXIS2_PLACEMENT_3D ( 'NONE', #43752, #33924, #54660 ) ;
#62198=VERTEX_POINT ( 'NONE', #9644 ) ;
#62414=ORIENTED_EDGE ( 'NONE', *, *, #31005, .F. ) ;
#62508=CARTESIAN_POINT ( 'NONE',  ( 0.000000000000000000, 0.000000000000000000, 0.000000000000000000 ) ) ;
#62620=CARTESIAN_POINT ( 'NONE',  ( 0.000000000000000000, 6.928203230275506108, 4.000000000000007105 ) ) ;
#62625=LINE ( 'NONE', #4224, #60681 ) ;
#62643=CIRCLE ( 'NONE', #10946, 8.000000000000000000 ) ;
#62650=FILL_AREA_STYLE ('',( #20762 ) ) ;
#62696=CARTESIAN_POINT ( 'NONE',  ( 0.000000000000000000, 0.000000000000000000, 0.000000000000000000 ) ) ;
#62773=CARTESIAN_POINT ( 'NONE',  ( 0.000000000000000000, 0.000000000000000000, 8.000000000000000000 ) ) ;
#62801=CARTESIAN_POINT ( 'NONE',  ( 0.06809871960542744629, 7.710219529346611367, -2.645508037661881584 ) ) ;
#62806=EDGE_CURVE ( 'NONE', #43392, #20959, #28873, .T. ) ;
#62911=EDGE_CURVE ( 'NONE', #36977, #2227, #39841, .T. ) ;
#63215=DIRECTION ( 'NONE',  ( -1.000000000000000000, -0.000000000000000000, -0.000000000000000000 ) ) ;
#63269=DIRECTION ( 'NONE',  ( -0.000000000000000000, 0.000000000000000000, 1.000000000000000000 ) ) ;
#63301=DIRECTION ( 'NONE',  ( 0.000000000000000000, 0.000000000000000000, -1.000000000000000000 ) ) ;
#63441=CARTESIAN_POINT ( 'NONE',  ( 0.3194001229790394136, 3.115132258388581210, 7.999999999999998224 ) ) ;
#63443=DIRECTION ( 'NONE',  ( -1.000000000000000000, -0.000000000000000000, 0.000000000000000000 ) ) ;
#63502=ADVANCED_FACE ( 'NONE', ( #49780 ), #53999, .F. ) ;
#63515=DIRECTION ( 'NONE',  ( 0.000000000000000000, 0.000000000000000000, -1.000000000000000000 ) ) ;
#63621=B_SPLINE_CURVE_WITH_KNOTS ( 'NONE', 3,
 ( #30699, #33645, #6893, #40552, #41259, #28350 ),
 .UNSPECIFIED., .F., .F.,
 ( 4, 2, 4 ),
 ( 2.380731629582122378E-07, 0.002336973833157553367, 0.004673709593152147908 ),
 .UNSPECIFIED. ) ;
#63640=CONICAL_SURFACE ( 'NONE', #54628, 4.171999999999999709, 0.7853981633974437271 ) ;
#63698=EDGE_CURVE ( 'NONE', #62198, #43392, #16133, .T. ) ;
#63748=ORIENTED_EDGE ( 'NONE', *, *, #13270, .F. ) ;
#63780=ORIENTED_EDGE ( 'NONE', *, *, #12961, .F. ) ;
#63974=CARTESIAN_POINT ( 'NONE',  ( 0.000000000000000000, -6.928203230275509661, -3.999999999999999112 ) ) ;
#64027=LINE ( 'NONE', #338, #10987 ) ;
#64123=CARTESIAN_POINT ( 'NONE',  ( 6.400000000000000355, 4.618802153517004960, 7.999999999999998224 ) ) ;
#64179=ORIENTED_EDGE ( 'NONE', *, *, #6934, .F. ) ;
#64290=CIRCLE ( 'NONE', #33971, 8.000000000000000000 ) ;
#64466=CARTESIAN_POINT ( 'NONE',  ( -9.929343724188531780E-16, 0.3912769056150340319, 8.000000000000000000 ) ) ;
#64589=DIRECTION ( 'NONE',  ( 1.000000000000000000, 0.000000000000000000, 0.000000000000000000 ) ) ;
#64648=APPLICATION_CONTEXT ( 'automotive_design' ) ;
#64651=ORIENTED_EDGE ( 'NONE', *, *, #48317, .T. ) ;
#64745=ORIENTED_EDGE ( 'NONE', *, *, #31320, .T. ) ;
#64753=DIRECTION ( 'NONE',  ( 0.000000000000000000, 0.000000000000000000, 1.000000000000000000 ) ) ;
#64821=FACE_OUTER_BOUND ( 'NONE', #32282, .T. ) ;
#64826=DIRECTION ( 'NONE',  ( 0.000000000000000000, 0.000000000000000000, -1.000000000000000000 ) ) ;
#64876=AXIS2_PLACEMENT_3D ( 'NONE', #52429, #41532, #24673 ) ;
#64959=EDGE_CURVE ( 'NONE', #46646, #6777, #11767, .T. ) ;
#65079=DIRECTION ( 'NONE',  ( -1.000000000000000000, -0.000000000000000000, -0.000000000000000000 ) ) ;
#65089=EDGE_LOOP ( 'NONE', ( #13651, #29946, #69548, #27134, #14405, #48609 ) ) ;
#65096=CARTESIAN_POINT ( 'NONE',  ( 0.3167204509598202655, -5.377136764700215288, -6.686525924292707757 ) ) ;
#65193=EDGE_CURVE ( 'NONE', #20959, #21223, #30227, .T. ) ;
#65231=DIRECTION ( 'NONE',  ( 1.000000000000000000, 0.000000000000000000, -0.000000000000000000 ) ) ;
#65341=ADVANCED_FACE ( 'NONE', ( #64821 ), #67404, .F. ) ;
#65627=ORIENTED_EDGE ( 'NONE', *, *, #14292, .F. ) ;
#65989=DIRECTION ( 'NONE',  ( -0.000000000000000000, 1.000000000000000000, -1.224646799147353207E-16 ) ) ;
#66048=LINE ( 'NONE', #55465, #42429 ) ;
#66261=B_SPLINE_CURVE_WITH_KNOTS ( 'NONE', 3,
 ( #17685, #55657, #50035, #22958, #11695, #1151 ),
 .UNSPECIFIED., .F., .F.,
 ( 4, 2, 4 ),
 ( 2.380731629584203697E-07, 0.002336973833157565510, 0.004673709593152172194 ),
 .UNSPECIFIED. ) ;
#66452=ORIENTED_EDGE ( 'NONE', *, *, #62806, .F. ) ;
#66603=VERTEX_POINT ( 'NONE', #16204 ) ;
#66770=ORIENTED_EDGE ( 'NONE', *, *, #55836, .T. ) ;
#66832=AXIS2_PLACEMENT_3D ( 'NONE', #50530, #44558, #8319 ) ;
#66892=ADVANCED_FACE ( 'NONE', ( #52383 ), #37274, .T. ) ;
#66953=FACE_OUTER_BOUND ( 'NONE', #36260, .T. ) ;
#67299=ORIENTED_EDGE ( 'NONE', *, *, #36787, .T. ) ;
#67404=TOROIDAL_SURFACE ( 'NONE', #24723, 5.400000000000001243, 0.4000000000000000222 ) ;
#67495=LINE ( 'NONE', #56942, #31104 ) ;
#67567=CIRCLE ( 'NONE', #33866, 5.000000000000000888 ) ;
#67601=CARTESIAN_POINT ( 'NONE',  ( 6.400000000000000355, 0.000000000000000000, 0.000000000000000000 ) ) ;
#67612=CIRCLE ( 'NONE', #50729, 5.000000000000000888 ) ;
#67711=DIRECTION ( 'NONE',  ( -1.000000000000000000, -0.000000000000000000, -0.000000000000000000 ) ) ;
#67799=EDGE_LOOP ( 'NONE', ( #59469, #50219, #102, #66452, #18052, #21675 ) ) ;
#67952=DIRECTION ( 'NONE',  ( 0.000000000000000000, 0.000000000000000000, -1.000000000000000000 ) ) ;
#68079=AXIS2_PLACEMENT_3D ( 'NONE', #13061, #60538, #49267 ) ;
#68097=DIRECTION ( 'NONE',  ( 0.000000000000000000, 0.000000000000000000, -1.000000000000000000 ) ) ;
#68115=DIRECTION ( 'NONE',  ( -1.000000000000000000, -0.000000000000000000, -0.000000000000000000 ) ) ;
#68255=ORIENTED_EDGE ( 'NONE', *, *, #20792, .T. ) ;
#68312=VERTEX_POINT ( 'NONE', #33998 ) ;
#68355=AXIS2_PLACEMENT_3D ( 'NONE', #32635, #4181, #63269 ) ;
#68417=ORIENTED_EDGE ( 'NONE', *, *, #60509, .F. ) ;
#68463=ORIENTED_EDGE ( 'NONE', *, *, #37017, .T. ) ;
#68542=LINE ( 'NONE', #19659, #22567 ) ;
#68605=SURFACE_STYLE_USAGE ( .BOTH. , #3902 ) ;
#68661=EDGE_CURVE ( 'NONE', #15138, #38316, #24088, .T. ) ;
#68847=DIRECTION ( 'NONE',  ( 1.000000000000000000, 0.000000000000000000, -0.000000000000000000 ) ) ;
#68924=DIRECTION ( 'NONE',  ( 0.000000000000000000, 0.000000000000000000, 1.000000000000000000 ) ) ;
#68937=VECTOR ( 'NONE', #18705, 1000.000000000000000 ) ;
#69024=CARTESIAN_POINT ( 'NONE',  ( 51.39999999999999858, 5.109226446042757607E-16, -4.171999999999999709 ) ) ;
#69105=VERTEX_POINT ( 'NONE', #48489 ) ;
#69266=ADVANCED_FACE ( 'NONE', ( #36858 ), #47389, .F. ) ;
#69273=ORIENTED_EDGE ( 'NONE', *, *, #35169, .T. ) ;
#69548=ORIENTED_EDGE ( 'NONE', *, *, #18928, .F. ) ;
ENDSEC;
END-ISO-10303-21;
